ISO-10303-21;
HEADER;
FILE_DESCRIPTION (('STEP AP214'),
    '1' );
FILE_NAME ('hex flange nut gradea_iso_ISO - 4161 - M10 - N.step',
    '2026-10-31T03:46:07',
    ( '' ),
    ( '' ),
    'SwSTEP 2.0',
    'SolidWorks 2026',
    '' );
FILE_SCHEMA (( 'AUTOMOTIVE_DESIGN' ));
ENDSEC;

DATA;
#20=ORIENTED_EDGE ( 'NONE', *, *, #18012, .T. ) ;
#30=CARTESIAN_POINT ( 'NONE',  ( -3.096526599377909417, 6.872473572140716414, 1.143494478793305063E-15 ) ) ;
#65=CARTESIAN_POINT ( 'NONE',  ( -7.500000000000000000, 4.330127018922191873, -0.9999999999999970024 ) ) ;
#66=CARTESIAN_POINT ( 'NONE',  ( 1.249999999999999112, -7.938566201357367902, -7.198902722707431145 ) ) ;
#70=CARTESIAN_POINT ( 'NONE',  ( 7.499999999999999112, 0.7513028741560161539, -0.02472015219302839059 ) ) ;
#95=CARTESIAN_POINT ( 'NONE',  ( -0.2779000157839473517, -8.820699686765063774, -7.928862157988305626 ) ) ;
#100=DIRECTION ( 'NONE',  ( 0.000000000000000000, 0.000000000000000000, 1.000000000000000000 ) ) ;
#135=ADVANCED_FACE ( 'NONE', ( #19802 ), #12982, .T. ) ;
#162=CARTESIAN_POINT ( 'NONE',  ( 4.999999999999999112, 5.773502691896256422, -7.063244554129997965 ) ) ;
#199=DIRECTION ( 'NONE',  ( -0.000000000000000000, -0.000000000000000000, 1.000000000000000000 ) ) ;
#201=CARTESIAN_POINT ( 'NONE',  ( -7.500000000000000000, -4.732323933430407692, -7.493854309896101462 ) ) ;
#216=CARTESIAN_POINT ( 'NONE',  ( -6.127431526422343306E-17, 9.147862274876549904, -8.047472243342932430 ) ) ;
#219=EDGE_CURVE ( 'NONE', #14233, #9344, #13241, .T. ) ;
#246=CARTESIAN_POINT ( 'NONE',  ( -0.6508621380849236582, -8.763657152406455708, -7.907633014911225722 ) ) ;
#306=VERTEX_POINT ( 'NONE', #2634 ) ;
#307=AXIS2_PLACEMENT_3D ( 'NONE', #11338, #18648, #9749 ) ;
#309=LINE ( 'NONE', #9020, #16498 ) ;
#353=EDGE_CURVE ( 'NONE', #6861, #5614, #602, .T. ) ;
#370=( GEOMETRIC_REPRESENTATION_CONTEXT ( 3 ) GLOBAL_UNCERTAINTY_ASSIGNED_CONTEXT ( ( #3597 ) ) GLOBAL_UNIT_ASSIGNED_CONTEXT ( ( #16013, #5250, #17687 ) ) REPRESENTATION_CONTEXT ( 'NONE', 'WORKASPACE' ) );
#390=CARTESIAN_POINT ( 'NONE',  ( -2.621328321948020346, -7.606199919102354379, -7.633618187056584681 ) ) ;
#425=CARTESIAN_POINT ( 'NONE',  ( -7.808218555863076560, -4.508077085118260108, -7.999534413642739317 ) ) ;
#429=DIRECTION ( 'NONE',  ( 1.000000000000000000, 0.000000000000000000, 0.000000000000000000 ) ) ;
#438=EDGE_LOOP ( 'NONE', ( #2564, #18535, #16331, #17090, #23545 ) ) ;
#465=ORIENTED_EDGE ( 'NONE', *, *, #13801, .F. ) ;
#482=CARTESIAN_POINT ( 'NONE',  ( -6.902527771671634227, -4.675077770780906583, -0.7026937717022867513 ) ) ;
#499=DIRECTION ( 'NONE',  ( 0.000000000000000000, 0.000000000000000000, 1.000000000000000000 ) ) ;
#538=CARTESIAN_POINT ( 'NONE',  ( 0.000000000000000000, 0.000000000000000000, -9.974600000000000577 ) ) ;
#551=CARTESIAN_POINT ( 'NONE',  ( 7.500000000000000000, 4.330127018922199866, -1.000000000000000888 ) ) ;
#602=CIRCLE ( 'NONE', #4405, 0.7733184030943203169 ) ;
#620=CARTESIAN_POINT ( 'NONE',  ( -5.335963852939856089, -6.035591050534137025, -7.593821156097342318 ) ) ;
#639=LINE ( 'NONE', #8009, #11174 ) ;
#673=CARTESIAN_POINT ( 'NONE',  ( -7.894706624614703294, -0.7534108004380160040, -7.590222617908770175 ) ) ;
#690=CIRCLE ( 'NONE', #14219, 5.000000000000000888 ) ;
#692=VECTOR ( 'NONE', #7161, 1000.000000000000000 ) ;
#737=MECHANICAL_DESIGN_GEOMETRIC_PRESENTATION_REPRESENTATION('',(#8859),#11190);
#768=CARTESIAN_POINT ( 'NONE',  ( 7.908230272950877549, -3.123266379887881250, -7.776722524729575703 ) ) ;
#771=PLANE ( 'NONE',  #4084 ) ;
#780=ORIENTED_EDGE ( 'NONE', *, *, #3573, .F. ) ;
#781=AXIS2_PLACEMENT_3D ( 'NONE', #12948, #7112, #5536 ) ;
#833=ORIENTED_EDGE ( 'NONE', *, *, #925, .F. ) ;
#847=CARTESIAN_POINT ( 'NONE',  ( -7.968863443239230016, -4.547634245050486079, -8.057411785091789014 ) ) ;
#876=CARTESIAN_POINT ( 'NONE',  ( 7.500000000000000000, 1.572594658376109011, -7.069792055233639516 ) ) ;
#925=EDGE_CURVE ( 'NONE', #23462, #21875, #23659, .T. ) ;
#928=DIRECTION ( 'NONE',  ( -1.000000000000000000, 1.224646799147354686E-16, 0.000000000000000000 ) ) ;
#929=EDGE_LOOP ( 'NONE', ( #19445, #20802, #6754, #17160, #13863 ) ) ;
#986=FACE_OUTER_BOUND ( 'NONE', #1753, .T. ) ;
#999=EDGE_CURVE ( 'NONE', #6769, #306, #21098, .T. ) ;
#1012=CARTESIAN_POINT ( 'NONE',  ( 3.096526599377912525, -6.872473572140722631, -5.976664475826341615E-15 ) ) ;
#1029=DIRECTION ( 'NONE',  ( 1.000000000000000000, 0.000000000000000000, 0.000000000000000000 ) ) ;
#1039=ADVANCED_FACE ( 'NONE', ( #3145 ), #6781, .T. ) ;
#1041=CARTESIAN_POINT ( 'NONE',  ( -6.875000000000001776, -4.690970937165714894, -7.298562697733108173 ) ) ;
#1110=EDGE_LOOP ( 'NONE', ( #18474, #16376, #16374, #13922 ) ) ;
#1116=CARTESIAN_POINT ( 'NONE',  ( 7.500000000000000000, -4.730916290271713898, -7.493595886788494198 ) ) ;
#1125=ORIENTED_EDGE ( 'NONE', *, *, #353, .F. ) ;
#1150=EDGE_CURVE ( 'NONE', #7557, #1864, #19432, .T. ) ;
#1163=CONICAL_SURFACE ( 'NONE', #10852, 5.000000000000001776, 0.9599310885968795892 ) ;
#1175=ADVANCED_FACE ( 'NONE', ( #23193 ), #14559, .F. ) ;
#1184=ORIENTED_EDGE ( 'NONE', *, *, #3190, .F. ) ;
#1196=CARTESIAN_POINT ( 'NONE',  ( 1.206569728928466700, 7.963640680051486953, -0.4524126574264497602 ) ) ;
#1199=EDGE_CURVE ( 'NONE', #21582, #14233, #11844, .T. ) ;
#1209=CARTESIAN_POINT ( 'NONE',  ( -2.558993250147282073, 7.638875775587784744, -7.593821156097241065 ) ) ;
#1210=DIRECTION ( 'NONE',  ( -0.000000000000000000, -0.000000000000000000, 1.000000000000000000 ) ) ;
#1220=CARTESIAN_POINT ( 'NONE',  ( 5.147825380264231754, 5.688155668806028409, -7.450218641347809090 ) ) ;
#1235=EDGE_CURVE ( 'NONE', #9811, #1621, #11604, .T. ) ;
#1237=CARTESIAN_POINT ( 'NONE',  ( -1.250000000000000444, 7.938566201357357244, -7.198902722707429369 ) ) ;
#1240=CARTESIAN_POINT ( 'NONE',  ( 0.000000000000000000, 0.000000000000000000, 0.000000000000000000 ) ) ;
#1318=CARTESIAN_POINT ( 'NONE',  ( 0.3470952277635277472, 8.860649561028097310, -7.493596212620242447 ) ) ;
#1335=FACE_OUTER_BOUND ( 'NONE', #15483, .T. ) ;
#1341=CARTESIAN_POINT ( 'NONE',  ( 7.500000000000000000, -4.330127018922199866, -7.422398894150035176 ) ) ;
#1361=CARTESIAN_POINT ( 'NONE',  ( 7.500000000000000000, -3.988190556646209028, -0.8526458641284331286 ) ) ;
#1369=ORIENTED_EDGE ( 'NONE', *, *, #15166, .T. ) ;
#1384=SURFACE_SIDE_STYLE ('',( #14555 ) ) ;
#1385=FACE_OUTER_BOUND ( 'NONE', #21095, .T. ) ;
#1386=CARTESIAN_POINT ( 'NONE',  ( 3.749999999999999112, -6.495190528383302464, -6.991905250253757309 ) ) ;
#1388=ORIENTED_EDGE ( 'NONE', *, *, #20616, .F. ) ;
#1400=CARTESIAN_POINT ( 'NONE',  ( 0.000000000000000000, 0.000000000000000000, -0.5251556536572846712 ) ) ;
#1447=FACE_OUTER_BOUND ( 'NONE', #2462, .T. ) ;
#1449=CARTESIAN_POINT ( 'NONE',  ( 2.411464220263165092, 7.267994521134541586, -7.491772860716163329 ) ) ;
#1502=DIRECTION ( 'NONE',  ( -0.000000000000000000, -0.000000000000000000, 1.000000000000000000 ) ) ;
#1508=PLANE ( 'NONE',  #10688 ) ;
#1529=CARTESIAN_POINT ( 'NONE',  ( -4.406842699996122548, 6.115962218725288224, 1.165517335421917267E-15 ) ) ;
#1563=ORIENTED_EDGE ( 'NONE', *, *, #18137, .T. ) ;
#1569=CARTESIAN_POINT ( 'NONE',  ( 0.2779000157839532359, 8.820699686765054892, -7.928862157988302961 ) ) ;
#1575=DIRECTION ( 'NONE',  ( -0.000000000000000000, -0.000000000000000000, 1.000000000000000000 ) ) ;
#1621=VERTEX_POINT ( 'NONE', #14596 ) ;
#1632=DIRECTION ( 'NONE',  ( 1.000000000000000000, 0.000000000000000000, 0.000000000000000000 ) ) ;
#1693=CARTESIAN_POINT ( 'NONE',  ( 7.500000000000001776, 0.000000000000000000, 0.000000000000000000 ) ) ;
#1727=CARTESIAN_POINT ( 'NONE',  ( 7.908030677224553884, -3.059924800338349904, -7.792662696733364314 ) ) ;
#1749=CARTESIAN_POINT ( 'NONE',  ( 5.000000000000001776, 6.123233995736768255E-16, -9.974600000000000577 ) ) ;
#1753=EDGE_LOOP ( 'NONE', ( #14529, #14866, #3158, #19813, #833 ) ) ;
#1795=CARTESIAN_POINT ( 'NONE',  ( -6.127431526422343306E-17, 9.147862274876549904, -8.047472243342932430 ) ) ;
#1824=ORIENTED_EDGE ( 'NONE', *, *, #17434, .T. ) ;
#1844=CARTESIAN_POINT ( 'NONE',  ( -5.007715329123872641E-16, -8.660254037844399733, -7.422398894150038728 ) ) ;
#1853=DIRECTION ( 'NONE',  ( 1.000000000000000000, 0.000000000000000000, 0.000000000000000000 ) ) ;
#1858=CONICAL_SURFACE ( 'NONE', #8061, 7.500000000000001776, 0.8594454914424796144 ) ;
#1860=VECTOR ( 'NONE', #5273, 1000.000000000000114 ) ;
#1861=DIRECTION ( 'NONE',  ( 0.000000000000000000, 0.000000000000000000, -1.000000000000000000 ) ) ;
#1864=VERTEX_POINT ( 'NONE', #12196 ) ;
#1870=PLANE ( 'NONE',  #10772 ) ;
#1881=CARTESIAN_POINT ( 'NONE',  ( 7.298354728637812983, -4.926141412639873707, -7.913704048099693189 ) ) ;
#1891=CARTESIAN_POINT ( 'NONE',  ( 4.606548227981508425, 6.456511556909250160, -7.591235721156633254 ) ) ;
#1909=B_SPLINE_CURVE_WITH_KNOTS ( 'NONE', 3,
 ( #216, #13185, #11110, #22420, #20486, #1891, #13291, #9517, #3581, #10997 ),
 .UNSPECIFIED., .F., .F.,
 ( 4, 2, 2, 2, 4 ),
 ( 1.572453990175171705E-19, 0.002305503304226491201, 0.004611006608452982401, 0.006916509912679473168, 0.009222013216905964803 ),
 .UNSPECIFIED. ) ;
#1985=ORIENTED_EDGE ( 'NONE', *, *, #3573, .T. ) ;
#1987=DIRECTION ( 'NONE',  ( 1.000000000000000000, 0.000000000000000000, 0.000000000000000000 ) ) ;
#1994=CARTESIAN_POINT ( 'NONE',  ( 7.500000000000000000, -4.330127018922199866, -7.422398894150035176 ) ) ;
#2004=FACE_OUTER_BOUND ( 'NONE', #4666, .T. ) ;
#2049=DIRECTION ( 'NONE',  ( 0.000000000000000000, 0.000000000000000000, 1.000000000000000000 ) ) ;
#2058=CARTESIAN_POINT ( 'NONE',  ( -7.922281120364393914, 4.573931137438271399, -8.047472243342930653 ) ) ;
#2087=CARTESIAN_POINT ( 'NONE',  ( -7.703920929261754758, -4.447860822324869901, -7.917989418073284824 ) ) ;
#2135=PRODUCT_CONTEXT ( 'NONE', #11093, 'mechanical' ) ;
#2220=AXIS2_PLACEMENT_3D ( 'NONE', #8767, #1502, #23485 ) ;
#2231=FACE_OUTER_BOUND ( 'NONE', #16287, .T. ) ;
#2301=FACE_OUTER_BOUND ( 'NONE', #15644, .T. ) ;
#2346=VERTEX_POINT ( 'NONE', #19589 ) ;
#2382=EDGE_CURVE ( 'NONE', #1621, #19296, #10822, .T. ) ;
#2386=CARTESIAN_POINT ( 'NONE',  ( 0.000000000000000000, 0.000000000000000000, 0.000000000000000000 ) ) ;
#2414=CYLINDRICAL_SURFACE ( 'NONE', #20904, 4.250000000000000000 ) ;
#2418=CARTESIAN_POINT ( 'NONE',  ( -0.6169862416623524970, -8.783631307150855605, -7.913704048099795330 ) ) ;
#2419=VECTOR ( 'NONE', #1210, 1000.000000000000000 ) ;
#2439=CARTESIAN_POINT ( 'NONE',  ( 1.250000000000000222, 7.938566201357357244, -7.198902722707428481 ) ) ;
#2449=CARTESIAN_POINT ( 'NONE',  ( -7.500000000000000000, -4.330127018922198090, -7.422398894150034288 ) ) ;
#2462=EDGE_LOOP ( 'NONE', ( #9554, #19199, #18103 ) ) ;
#2479=CARTESIAN_POINT ( 'NONE',  ( -7.500000000000000000, 4.730921838224027454, -7.493596905200499592 ) ) ;
#2526=PLANE ( 'NONE',  #3593 ) ;
#2564=ORIENTED_EDGE ( 'NONE', *, *, #22136, .F. ) ;
#2572=ORIENTED_EDGE ( 'NONE', *, *, #6969, .T. ) ;
#2611=CARTESIAN_POINT ( 'NONE',  ( -3.750000000000007105, -6.495190528383289141, 0.000000000000000000 ) ) ;
#2634=CARTESIAN_POINT ( 'NONE',  ( 7.500000000000000000, 4.330127018922199866, -1.000000000000000888 ) ) ;
#2661=CARTESIAN_POINT ( 'NONE',  ( -3.080866544137490504, -6.881514909249304424, -7.026396753507435200 ) ) ;
#2675=AXIS2_PLACEMENT_3D ( 'NONE', #1240, #6317, #19231 ) ;
#2703=CARTESIAN_POINT ( 'NONE',  ( -0.6250000000000001110, 8.299410119600874935, -7.298562697733108173 ) ) ;
#2705=DIRECTION ( 'NONE',  ( 0.000000000000000000, 0.000000000000000000, 1.000000000000000000 ) ) ;
#2717=ORIENTED_EDGE ( 'NONE', *, *, #22537, .T. ) ;
#2721=CARTESIAN_POINT ( 'NONE',  ( 6.902527771671632451, 4.675077770780898589, -0.7026937717022819774 ) ) ;
#2744=VERTEX_POINT ( 'NONE', #23196 ) ;
#2752=CARTESIAN_POINT ( 'NONE',  ( -5.000000000000000888, 6.123233995736767268E-16, -10.00000000000000000 ) ) ;
#2758=CARTESIAN_POINT ( 'NONE',  ( -3.823040241140506157E-16, -8.660254037844397956, -7.564338275809345369 ) ) ;
#2767=FACE_BOUND ( 'NONE', #7448, .T. ) ;
#2775=CARTESIAN_POINT ( 'NONE',  ( -6.484173630544109557, -4.916614646775610886, -7.642786413610934915 ) ) ;
#2785=CARTESIAN_POINT ( 'NONE',  ( 0.000000000000000000, 0.000000000000000000, 0.000000000000000000 ) ) ;
#2802=CARTESIAN_POINT ( 'NONE',  ( 7.499999999998625100, 3.882635837268474166, -7.781684861371460649 ) ) ;
#2857=ORIENTED_EDGE ( 'NONE', *, *, #13639, .F. ) ;
#2901=CARTESIAN_POINT ( 'NONE',  ( -3.288228914120473245, 7.217643567644804747, -7.591235721156635030 ) ) ;
#2938=DIRECTION ( 'NONE',  ( -0.000000000000000000, -0.000000000000000000, 1.000000000000000000 ) ) ;
#2977=ADVANCED_FACE ( 'NONE', ( #22536 ), #17691, .T. ) ;
#2997=DIRECTION ( 'NONE',  ( -0.000000000000000000, -0.000000000000000000, 1.000000000000000000 ) ) ;
#3013=CARTESIAN_POINT ( 'NONE',  ( 6.484173630542770184, 4.916614646782027087, -7.642786413619098163 ) ) ;
#3145=FACE_OUTER_BOUND ( 'NONE', #6804, .T. ) ;
#3158=ORIENTED_EDGE ( 'NONE', *, *, #19479, .F. ) ;
#3176=ORIENTED_EDGE ( 'NONE', *, *, #12128, .F. ) ;
#3190=EDGE_CURVE ( 'NONE', #23656, #7557, #4578, .T. ) ;
#3193=CARTESIAN_POINT ( 'NONE',  ( -14.99999999999998934, -1.734723475976807094E-15, -10.00000000000000000 ) ) ;
#3205=CARTESIAN_POINT ( 'NONE',  ( 4.406842699996126989, -6.115962218725295330, -6.291760732204942919E-15 ) ) ;
#3216=ORIENTED_EDGE ( 'NONE', *, *, #10905, .T. ) ;
#3243=AXIS2_PLACEMENT_3D ( 'NONE', #3253, #1575, #17998 ) ;
#3252=( BOUNDED_SURFACE ( )  B_SPLINE_SURFACE ( 3, 2, ( 
 ( #6042, #17049, #847 ),
 ( #7982, #2775, #11762 ),
 ( #11882, #6406, #620 ),
 ( #2661, #18955, #21135 ),
 ( #20899, #11651, #390 ),
 ( #13811, #22820, #10059 ),
 ( #9927, #7753, #2418 ),
 ( #9806, #17161, #22702 ) ),
 .UNSPECIFIED., .F., .F., .F. ) 
 B_SPLINE_SURFACE_WITH_KNOTS ( ( 4, 2, 2, 4 ),
 ( 3, 3 ),
 ( 0.03861844051980971304, 0.04325213341840642572, 0.04556897986770477860, 0.04788582631700313841 ),
 ( 0.000000000000000000, 1.000000000000000000 ),
 .UNSPECIFIED. ) 
 GEOMETRIC_REPRESENTATION_ITEM ( )  RATIONAL_B_SPLINE_SURFACE ( (
 ( 1.000000000000000000, 0.8047781759831923454, 1.000000000000000000),
 ( 1.000000000000000000, 0.8123762462805160789, 1.000000000000000000),
 ( 1.000000000000000000, 0.8190659850616602844, 1.000000000000000000),
 ( 1.000000000000000000, 0.8191937571013702124, 1.000000000000000000),
 ( 1.000000000000000000, 0.8176092952780309453, 1.000000000000000000),
 ( 1.000000000000000000, 0.8122962088596628050, 1.000000000000000000),
 ( 1.000000000000000000, 0.8086311330827828936, 1.000000000000000000),
 ( 1.000000000000000000, 0.8047712282214327661, 1.000000000000000000) ) ) 
 REPRESENTATION_ITEM ( '' )  SURFACE ( )  );
#3253=CARTESIAN_POINT ( 'NONE',  ( 0.000000000000000000, 0.000000000000000000, -9.226681596905677907 ) ) ;
#3257=DIRECTION ( 'NONE',  ( -1.000000000000000000, 0.000000000000000000, 0.000000000000000000 ) ) ;
#3265=DIRECTION ( 'NONE',  ( 0.000000000000000000, 0.000000000000000000, -1.000000000000000000 ) ) ;
#3285=CARTESIAN_POINT ( 'NONE',  ( 3.750000000000005329, 6.495190528383288253, 0.000000000000000000 ) ) ;
#3304=VECTOR ( 'NONE', #13953, 1000.000000000000114 ) ;
#3312=FACE_OUTER_BOUND ( 'NONE', #4071, .T. ) ;
#3342=CARTESIAN_POINT ( 'NONE',  ( 7.112481253774308954, -4.553861071371678726, -7.781689322728511549 ) ) ;
#3372=CARTESIAN_POINT ( 'NONE',  ( -0.2791032213812780771, 8.821394357840562250, -7.929128246061909024 ) ) ;
#3386=CARTESIAN_POINT ( 'NONE',  ( -7.500000000000000888, -3.640541674360520119, -0.7158139487964623182 ) ) ;
#3387=ORIENTED_EDGE ( 'NONE', *, *, #10710, .F. ) ;
#3398=ADVANCED_FACE ( 'NONE', ( #12553, #19868 ), #21220, .F. ) ;
#3399=AXIS2_PLACEMENT_3D ( 'NONE', #22275, #199, #18195 ) ;
#3419=DIRECTION ( 'NONE',  ( -1.000000000000000000, 0.000000000000000000, 0.000000000000000000 ) ) ;
#3425=DIRECTION ( 'NONE',  ( 1.000000000000000000, 0.000000000000000000, 0.000000000000000000 ) ) ;
#3542=CARTESIAN_POINT ( 'NONE',  ( -7.500000000000000888, 3.988838049906426875, -0.8529248949437632232 ) ) ;
#3558=CARTESIAN_POINT ( 'NONE',  ( -3.750000000000004885, 6.495190528383289141, 0.000000000000000000 ) ) ;
#3573=EDGE_CURVE ( 'NONE', #5614, #14374, #15040, .T. ) ;
#3580=B_SPLINE_CURVE_WITH_KNOTS ( 'NONE', 3,
 ( #19295, #2758, #8433, #21241, #23395, #4693 ),
 .UNSPECIFIED., .F., .F.,
 ( 4, 2, 4 ),
 ( 0.000000000000000000, 0.0004189869898914152461, 0.0008379739797828304922 ),
 .UNSPECIFIED. ) ;
#3581=CARTESIAN_POINT ( 'NONE',  ( 7.263825692932297962, 4.945657111639574666, -7.907570769506046204 ) ) ;
#3591=CARTESIAN_POINT ( 'NONE',  ( -6.439685834476978954, 4.942299687812971243, -7.659344964963200830 ) ) ;
#3593=AXIS2_PLACEMENT_3D ( 'NONE', #4819, #9914, #19182 ) ;
#3597=UNCERTAINTY_MEASURE_WITH_UNIT (LENGTH_MEASURE( 1.000000000000000082E-05 ), #16013, 'distance_accuracy_value', 'NONE');
#3600=ORIENTED_EDGE ( 'NONE', *, *, #16411, .T. ) ;
#3601=CARTESIAN_POINT ( 'NONE',  ( -2.352990130084580066E-16, 8.660254037844390851, -7.564335161054497547 ) ) ;
#3602=( GEOMETRIC_REPRESENTATION_CONTEXT ( 3 ) GLOBAL_UNCERTAINTY_ASSIGNED_CONTEXT ( ( #22799 ) ) GLOBAL_UNIT_ASSIGNED_CONTEXT ( ( #6970, #12561, #8917 ) ) REPRESENTATION_CONTEXT ( 'NONE', 'WORKASPACE' ) );
#3618=AXIS2_PLACEMENT_3D ( 'NONE', #18402, #1861, #1987 ) ;
#3626=EDGE_CURVE ( 'NONE', #6769, #17922, #17733, .T. ) ;
#3636=APPLICATION_CONTEXT ( 'automotive_design' ) ;
#3644=CLOSED_SHELL ( 'NONE', ( #5809, #5776, #21372, #12600, #135, #6832, #17905, #20973, #15146, #16611, #17623, #16392, #12431, #11501, #3398, #22865, #18846, #17040, #19591, #4140, #2977, #1039, #20660, #8312, #15858, #7874, #9616, #22930, #1175, #22832, #22592, #9292 ) ) ;
#3657=CARTESIAN_POINT ( 'NONE',  ( 7.499999999999999112, 0.3744244963005059490, 1.526918059583750369E-15 ) ) ;
#3688=CARTESIAN_POINT ( 'NONE',  ( 2.352174619736673744, -7.302225387959338399, -7.450218641350605076 ) ) ;
#3716=PRODUCT_DEFINITION_CONTEXT ( 'detailed design', #3636, 'design' ) ;
#3736=CARTESIAN_POINT ( 'NONE',  ( -2.459698528280933161, 7.240146430416066536, -0.09933465333851029810 ) ) ;
#3769=DIRECTION ( 'NONE',  ( 1.000000000000000000, 0.000000000000000000, 0.000000000000000000 ) ) ;
#3781=CARTESIAN_POINT ( 'NONE',  ( 7.500000000000002665, 3.988838049906435312, -0.8529248949437669980 ) ) ;
#3800=CARTESIAN_POINT ( 'NONE',  ( -7.549004593702459687, 4.358419834287835748, -7.700121441565839220 ) ) ;
#3803=CARTESIAN_POINT ( 'NONE',  ( -7.500000000000667910, 3.157052757790226316, -7.642767288269818771 ) ) ;
#3813=CARTESIAN_POINT ( 'NONE',  ( 7.779103221381273414, -4.168986698926031131, -7.929128246061905472 ) ) ;
#3833=CARTESIAN_POINT ( 'NONE',  ( 7.914973979435151463, 3.817460047930444134, -7.907502498112419786 ) ) ;
#3839=CARTESIAN_POINT ( 'NONE',  ( -5.276498195231978272, 6.073236878017963747, -7.633618187056680604 ) ) ;
#3970=CONICAL_SURFACE ( 'NONE', #5914, 10.39117206796836079, 1.221730476396047926 ) ;
#3979=LINE ( 'NONE', #11159, #20298 ) ;
#3981=ORIENTED_EDGE ( 'NONE', *, *, #18005, .T. ) ;
#3990=CARTESIAN_POINT ( 'NONE',  ( 0.000000000000000000, 0.000000000000000000, -9.449444346342714240 ) ) ;
#4006=ORIENTED_EDGE ( 'NONE', *, *, #10763, .F. ) ;
#4017=( BOUNDED_SURFACE ( )  B_SPLINE_SURFACE ( 3, 2, ( 
 ( #1318, #1569, #5433 ),
 ( #8951, #20145, #12368 ),
 ( #10413, #17764, #1209 ),
 ( #8580, #6760, #21487 ),
 ( #19680, #8699, #3839 ),
 ( #11256, #3591, #13196 ),
 ( #20499, #11479, #15212 ),
 ( #7359, #22185, #13302 ) ),
 .UNSPECIFIED., .F., .F., .T. ) 
 B_SPLINE_SURFACE_WITH_KNOTS ( ( 4, 2, 2, 4 ),
 ( 3, 3 ),
 ( 0.03861844051980969916, 0.04325213341840641879, 0.04556897986770477860, 0.04788582631700313841 ),
 ( 0.000000000000000000, 1.000000000000000000 ),
 .UNSPECIFIED. ) 
 GEOMETRIC_REPRESENTATION_ITEM ( )  RATIONAL_B_SPLINE_SURFACE ( (
 ( 1.000000000000000000, 0.8047781759831920123, 1.000000000000000000),
 ( 1.000000000000000000, 0.8123762462803147955, 1.000000000000000000),
 ( 1.000000000000000000, 0.8190659850619289584, 1.000000000000000000),
 ( 1.000000000000000000, 0.8191937571012362085, 1.000000000000000000),
 ( 1.000000000000000000, 0.8176092952779873135, 1.000000000000000000),
 ( 1.000000000000000000, 0.8122962088597077690, 1.000000000000000000),
 ( 1.000000000000000000, 0.8086311330827508081, 1.000000000000000000),
 ( 1.000000000000000000, 0.8047712282214326551, 1.000000000000000000) ) ) 
 REPRESENTATION_ITEM ( '' )  SURFACE ( )  );
#4056=VERTEX_POINT ( 'NONE', #16813 ) ;
#4071=EDGE_LOOP ( 'NONE', ( #22235, #7183, #21719, #11095, #23459 ) ) ;
#4084=AXIS2_PLACEMENT_3D ( 'NONE', #13732, #21052, #4510 ) ;
#4093=CARTESIAN_POINT ( 'NONE',  ( 0.000000000000000000, 0.000000000000000000, 0.000000000000000000 ) ) ;
#4095=DIRECTION ( 'NONE',  ( 1.000000000000000000, 0.000000000000000000, 0.000000000000000000 ) ) ;
#4105=AXIS2_PLACEMENT_3D ( 'NONE', #20043, #16318, #9063 ) ;
#4140=ADVANCED_FACE ( 'NONE', ( #1335 ), #14110, .T. ) ;
#4288=DIRECTION ( 'NONE',  ( -1.000000000000000000, 0.000000000000000000, 0.000000000000000000 ) ) ;
#4301=CARTESIAN_POINT ( 'NONE',  ( -7.500000000000000000, 3.202583086485915942, -7.213046687579523386 ) ) ;
#4336=VERTEX_POINT ( 'NONE', #19812 ) ;
#4345=ORIENTED_EDGE ( 'NONE', *, *, #353, .T. ) ;
#4357=ORIENTED_EDGE ( 'NONE', *, *, #1235, .F. ) ;
#4375=CARTESIAN_POINT ( 'NONE',  ( -6.127431526422343306E-17, 9.147862274876549904, -8.047472243342932430 ) ) ;
#4405=AXIS2_PLACEMENT_3D ( 'NONE', #10147, #23277, #19405 ) ;
#4474=CARTESIAN_POINT ( 'NONE',  ( 6.601567268551444378, -5.319966374295973743, -7.792327460285856766 ) ) ;
#4510=DIRECTION ( 'NONE',  ( 0.000000000000000000, 0.000000000000000000, 1.000000000000000000 ) ) ;
#4578=CIRCLE ( 'NONE', #22300, 4.250000000000000000 ) ;
#4579=ORIENTED_EDGE ( 'NONE', *, *, #2382, .F. ) ;
#4636=CARTESIAN_POINT ( 'NONE',  ( 7.922811941611899833, 4.628808333142401032, -8.057670691780701944 ) ) ;
#4653=CARTESIAN_POINT ( 'NONE',  ( -7.500000000000000000, 4.330127018922191873, -10.00000000000000000 ) ) ;
#4659=CARTESIAN_POINT ( 'NONE',  ( -7.922281120364393914, 4.573931137438271399, -8.047472243342930653 ) ) ;
#4666=EDGE_LOOP ( 'NONE', ( #18130, #15538, #11354, #22381 ) ) ;
#4676=DIRECTION ( 'NONE',  ( 0.000000000000000000, 0.000000000000000000, 1.000000000000000000 ) ) ;
#4693=CARTESIAN_POINT ( 'NONE',  ( -7.640563834021360018E-16, -9.147862274876560562, -8.047472243342937759 ) ) ;
#4705=CARTESIAN_POINT ( 'NONE',  ( -7.907996613752304782, -3.055722423191990611, -7.792112796859422374 ) ) ;
#4711=LINE ( 'NONE', #17765, #2419 ) ;
#4747=EDGE_LOOP ( 'NONE', ( #3387, #11767, #11004, #1824, #16928 ) ) ;
#4756=ORIENTED_EDGE ( 'NONE', *, *, #13639, .T. ) ;
#4773=SURFACE_STYLE_USAGE ( .BOTH. , #1384 ) ;
#4775=CARTESIAN_POINT ( 'NONE',  ( 7.500000000000000000, 4.330127018922190096, -10.00000000000000000 ) ) ;
#4781=MECHANICAL_DESIGN_GEOMETRIC_PRESENTATION_REPRESENTATION('',(#15609),#3602);
#4810=ORIENTED_EDGE ( 'NONE', *, *, #22437, .F. ) ;
#4819=CARTESIAN_POINT ( 'NONE',  ( -14.99999999999998934, -1.734723475976807094E-15, 0.000000000000000000 ) ) ;
#4840=CARTESIAN_POINT ( 'NONE',  ( 6.523606932381168733, 4.893847819346807348, -7.213065638943126245 ) ) ;
#4853=CARTESIAN_POINT ( 'NONE',  ( -0.6511518506208974211, 8.763486134561267349, -7.907570769506047981 ) ) ;
#4885=CARTESIAN_POINT ( 'NONE',  ( -7.894787914004607998, 0.7647108141804108694, -7.591390474663421095 ) ) ;
#4990=CIRCLE ( 'NONE', #8090, 4.250000000000000000 ) ;
#5025=( NAMED_UNIT ( * ) PLANE_ANGLE_UNIT ( ) SI_UNIT ( $, .RADIAN. ) );
#5032=CARTESIAN_POINT ( 'NONE',  ( -5.007715329123872641E-16, -8.660254037844399733, -10.00000000000000000 ) ) ;
#5045=CARTESIAN_POINT ( 'NONE',  ( -7.500000000000000000, 4.330127018922191873, -7.422398894150032511 ) ) ;
#5081=DIRECTION ( 'NONE',  ( 1.000000000000000000, 0.000000000000000000, 0.000000000000000000 ) ) ;
#5114=CARTESIAN_POINT ( 'NONE',  ( -2.352990130084580066E-16, 8.660254037844390851, -10.00000000000000000 ) ) ;
#5132=CARTESIAN_POINT ( 'NONE',  ( -7.500000000000000888, -3.608439182435167591, -7.298562697733108173 ) ) ;
#5149=EDGE_LOOP ( 'NONE', ( #12095, #20069, #780, #1125 ) ) ;
#5209=CARTESIAN_POINT ( 'NONE',  ( 10.39117206796836257, 0.000000000000000000, -8.499999999999998224 ) ) ;
#5231=FACE_OUTER_BOUND ( 'NONE', #22622, .T. ) ;
#5250=( NAMED_UNIT ( * ) PLANE_ANGLE_UNIT ( ) SI_UNIT ( $, .RADIAN. ) );
#5251=CARTESIAN_POINT ( 'NONE',  ( -7.500000000000000000, 4.330127018922191873, -7.422398894150032511 ) ) ;
#5271=CARTESIAN_POINT ( 'NONE',  ( -3.749999999999998224, -6.495190528383296247, -6.991905250253752868 ) ) ;
#5273=DIRECTION ( 'NONE',  ( 0.8191520442889907994, 1.003171929053523514E-16, -0.5735764363510474917 ) ) ;
#5278=LINE ( 'NONE', #16389, #8786 ) ;
#5303=DIRECTION ( 'NONE',  ( 1.000000000000000000, 0.000000000000000000, 0.000000000000000000 ) ) ;
#5308=B_SPLINE_CURVE_WITH_KNOTS ( 'NONE', 3,
 ( #1844, #5484, #66, #17935, #1386, #19737, #10715, #7416, #12436 ),
 .UNSPECIFIED., .F., .F.,
 ( 4, 2, 1, 2, 4 ),
 ( 6.245710625686469831E-20, 0.002165063509461098365, 0.004330127018922195863, 0.006495190528383293360, 0.008660254037844389990 ),
 .UNSPECIFIED. ) ;
#5316=DIRECTION ( 'NONE',  ( 1.000000000000000000, 0.000000000000000000, 0.000000000000000000 ) ) ;
#5373=CARTESIAN_POINT ( 'NONE',  ( -7.500000000000000000, 0.7513028741560130452, -0.02472015219302865774 ) ) ;
#5383=DIRECTION ( 'NONE',  ( -0.000000000000000000, -0.000000000000000000, 1.000000000000000000 ) ) ;
#5387=AXIS2_PLACEMENT_3D ( 'NONE', #21794, #11321, #1853 ) ;
#5418=VERTEX_POINT ( 'NONE', #6549 ) ;
#5421=CARTESIAN_POINT ( 'NONE',  ( 7.549006887134069643, 4.358421158401191597, -7.700127545397312367 ) ) ;
#5433=CARTESIAN_POINT ( 'NONE',  ( 0.04606493828584144051, 9.175055303659556571, -8.057411785091790790 ) ) ;
#5443=CARTESIAN_POINT ( 'NONE',  ( 1.013163106016871096, 8.075304045852551127, -7.231838333420561149 ) ) ;
#5484=CARTESIAN_POINT ( 'NONE',  ( 0.6249999999999994449, -8.299410119600885594, -7.298562697733110838 ) ) ;
#5505=CARTESIAN_POINT ( 'NONE',  ( -7.703920929261752981, 4.447860822324863683, -7.917989418073281271 ) ) ;
#5530=CARTESIAN_POINT ( 'NONE',  ( 7.500000000000000888, 4.330127018922190985, -7.564338275809340928 ) ) ;
#5532=ORIENTED_EDGE ( 'NONE', *, *, #16218, .F. ) ;
#5536=DIRECTION ( 'NONE',  ( 1.000000000000000000, 0.000000000000000000, 0.000000000000000000 ) ) ;
#5545=ORIENTED_EDGE ( 'NONE', *, *, #20225, .F. ) ;
#5549=CARTESIAN_POINT ( 'NONE',  ( 2.818872373871549124E-16, 8.716839668575678601, -7.700121441565840996 ) ) ;
#5595=DIRECTION ( 'NONE',  ( 0.000000000000000000, 0.000000000000000000, -1.000000000000000000 ) ) ;
#5597=DIRECTION ( 'NONE',  ( -0.000000000000000000, -0.000000000000000000, 1.000000000000000000 ) ) ;
#5612=ORIENTED_EDGE ( 'NONE', *, *, #7257, .F. ) ;
#5614=VERTEX_POINT ( 'NONE', #5209 ) ;
#5621=B_SPLINE_CURVE_WITH_KNOTS ( 'NONE', 3,
 ( #19529, #6993, #1196, #14485, #18209, #20013 ),
 .UNSPECIFIED., .F., .F.,
 ( 4, 2, 4 ),
 ( 2.475503369212747145E-07, 0.002222330217055634109, 0.004444412883774346255 ),
 .UNSPECIFIED. ) ;
#5635=DIRECTION ( 'NONE',  ( 0.000000000000000000, 0.000000000000000000, 1.000000000000000000 ) ) ;
#5640=CARTESIAN_POINT ( 'NONE',  ( 6.439685834477092641, -4.942299687812566233, -7.659344964963564983 ) ) ;
#5691=EDGE_LOOP ( 'NONE', ( #14828, #9992 ) ) ;
#5754=CARTESIAN_POINT ( 'NONE',  ( -7.499999999999653610, -1.545780083834116247, -7.491787297939224821 ) ) ;
#5776=ADVANCED_FACE ( 'NONE', ( #19541 ), #1163, .F. ) ;
#5809=ADVANCED_FACE ( 'NONE', ( #8578 ), #12236, .F. ) ;
#5816=CARTESIAN_POINT ( 'NONE',  ( -3.750000000000004885, 6.495190528383289141, 0.000000000000000000 ) ) ;
#5867=CARTESIAN_POINT ( 'NONE',  ( -7.915341292092594294, -3.857523022641989652, -7.913710289178173873 ) ) ;
#5892=EDGE_CURVE ( 'NONE', #6350, #21582, #17770, .T. ) ;
#5914=AXIS2_PLACEMENT_3D ( 'NONE', #13960, #3265, #7023 ) ;
#5922=CARTESIAN_POINT ( 'NONE',  ( -7.500000000000000000, -1.486698507076798847, -0.09861472150523968583 ) ) ;
#5970=VERTEX_POINT ( 'NONE', #11357 ) ;
#6006=DIRECTION ( 'NONE',  ( -1.000000000000000000, 0.000000000000000000, 0.000000000000000000 ) ) ;
#6042=CARTESIAN_POINT ( 'NONE',  ( -7.847095227763516867, -4.129731495738496960, -7.493596212620239783 ) ) ;
#6052=CARTESIAN_POINT ( 'NONE',  ( 7.500000000000000000, -4.330127018922199866, -7.422398894150035176 ) ) ;
#6092=CARTESIAN_POINT ( 'NONE',  ( 0.000000000000000000, 0.000000000000000000, -8.499999999999998224 ) ) ;
#6109=AXIS2_PLACEMENT_3D ( 'NONE', #8819, #14498, #5303 ) ;
#6171=CARTESIAN_POINT ( 'NONE',  ( 3.288228914120474133, -7.217643567644815406, -7.591235721156641247 ) ) ;
#6198=CARTESIAN_POINT ( 'NONE',  ( 7.500000000000000000, 4.330127018922190096, -7.422398894150032511 ) ) ;
#6208=CARTESIAN_POINT ( 'NONE',  ( -7.500000000000000888, -4.330127018922198090, -7.564335161054497547 ) ) ;
#6227=ORIENTED_EDGE ( 'NONE', *, *, #20849, .T. ) ;
#6246=EDGE_CURVE ( 'NONE', #12980, #16635, #16449, .T. ) ;
#6256=CARTESIAN_POINT ( 'NONE',  ( 0.000000000000000000, 0.000000000000000000, 0.000000000000000000 ) ) ;
#6258=VERTEX_POINT ( 'NONE', #18077 ) ;
#6296=CARTESIAN_POINT ( 'NONE',  ( 7.500000000000000888, 3.608439182435154269, -7.298562697733103732 ) ) ;
#6302=AXIS2_PLACEMENT_3D ( 'NONE', #9333, #14764, #14882 ) ;
#6315=CARTESIAN_POINT ( 'NONE',  ( -2.500000000000000000, 7.216878364870324525, -7.063244554130001518 ) ) ;
#6317=DIRECTION ( 'NONE',  ( 0.000000000000000000, 0.000000000000000000, 1.000000000000000000 ) ) ;
#6350=VERTEX_POINT ( 'NONE', #18193 ) ;
#6360=CARTESIAN_POINT ( 'NONE',  ( -10.12668159690567649, 1.256356190803088863E-15, -9.999999999999998224 ) ) ;
#6406=CARTESIAN_POINT ( 'NONE',  ( -5.147825380260782957, -5.688155668810408017, -7.450218641351304960 ) ) ;
#6413=AXIS2_PLACEMENT_3D ( 'NONE', #538, #7899, #429 ) ;
#6432=CARTESIAN_POINT ( 'NONE',  ( 7.897825807688775512, 1.532833846124499910, -7.633607627188418121 ) ) ;
#6496=PRODUCT ( 'hex flange nut gradea_iso_ISO - 4161 - M10 - N', 'hex flange nut gradea_iso_ISO - 4161 - M10 - N', '', ( #2135 ) ) ;
#6517=AXIS2_PLACEMENT_3D ( 'NONE', #19965, #5597, #3425 ) ;
#6542=B_SPLINE_CURVE_WITH_KNOTS ( 'NONE', 3,
 ( #5816, #30, #3736, #9202, #8966, #11154 ),
 .UNSPECIFIED., .F., .F.,
 ( 4, 2, 4 ),
 ( 0.004444412883774334112, 0.006655097293744431999, 0.008865781703714530754 ),
 .UNSPECIFIED. ) ;
#6544=AXIS2_PLACEMENT_3D ( 'NONE', #20106, #5383, #7307 ) ;
#6549=CARTESIAN_POINT ( 'NONE',  ( -5.000000000000001776, 0.000000000000000000, -9.974600000000000577 ) ) ;
#6651=ORIENTED_EDGE ( 'NONE', *, *, #20135, .T. ) ;
#6656=DIRECTION ( 'NONE',  ( 0.000000000000000000, 0.000000000000000000, 1.000000000000000000 ) ) ;
#6666=CARTESIAN_POINT ( 'NONE',  ( 7.703928834700302986, -4.447865386531950627, -7.917997657324739258 ) ) ;
#6671=CARTESIAN_POINT ( 'NONE',  ( -7.500000000000000000, -4.330127018922199866, -1.000000000000000888 ) ) ;
#6674=EDGE_CURVE ( 'NONE', #6350, #19296, #6542, .T. ) ;
#6754=ORIENTED_EDGE ( 'NONE', *, *, #8843, .T. ) ;
#6760=CARTESIAN_POINT ( 'NONE',  ( -4.406466114815342117, 6.116179640280717145, -7.446478553995464544 ) ) ;
#6769=VERTEX_POINT ( 'NONE', #1693 ) ;
#6777=CONICAL_SURFACE ( 'NONE', #7936, 10.39117206796836079, 1.221730476396047926 ) ;
#6781=CONICAL_SURFACE ( 'NONE', #16422, 7.500000000000001776, 0.8594454914424796144 ) ;
#6794=CARTESIAN_POINT ( 'NONE',  ( -6.250000000000000888, 5.051814855409225480, -7.198902722707429369 ) ) ;
#6802=CARTESIAN_POINT ( 'NONE',  ( 7.500000000000000000, -1.486698507076798847, -0.09861472150523931113 ) ) ;
#6804=EDGE_LOOP ( 'NONE', ( #4006, #18291, #11881 ) ) ;
#6826=CARTESIAN_POINT ( 'NONE',  ( -5.000000000000001776, 0.000000000000000000, -9.974600000000000577 ) ) ;
#6832=ADVANCED_FACE ( 'NONE', ( #18951 ), #2414, .F. ) ;
#6843=CARTESIAN_POINT ( 'NONE',  ( 6.901579824520443829, -4.675625068323827627, -0.7022220667781372549 ) ) ;
#6861=VERTEX_POINT ( 'NONE', #7857 ) ;
#6883=ORIENTED_EDGE ( 'NONE', *, *, #22437, .T. ) ;
#6940=DIRECTION ( 'NONE',  ( 1.000000000000000000, 0.000000000000000000, 0.000000000000000000 ) ) ;
#6947=CARTESIAN_POINT ( 'NONE',  ( 3.750000000000004441, -6.495190528383289141, 0.000000000000000000 ) ) ;
#6953=CARTESIAN_POINT ( 'NONE',  ( 7.894787914004607998, -0.7647108141804126458, -7.591390474663421095 ) ) ;
#6969=EDGE_CURVE ( 'NONE', #9811, #5970, #1909, .T. ) ;
#6970=( LENGTH_UNIT ( ) NAMED_UNIT ( * ) SI_UNIT ( .MILLI., .METRE. ) );
#6972=EDGE_LOOP ( 'NONE', ( #18172, #22521, #9916, #21648 ) ) ;
#6975=CARTESIAN_POINT ( 'NONE',  ( -2.499999999999999556, -7.216878364870334295, -7.063244554130003294 ) ) ;
#6993=CARTESIAN_POINT ( 'NONE',  ( 0.5984201754795568373, 8.314755988442765755, -0.7022220667781353676 ) ) ;
#7023=DIRECTION ( 'NONE',  ( -1.000000000000000000, 0.000000000000000000, 0.000000000000000000 ) ) ;
#7048=CARTESIAN_POINT ( 'NONE',  ( 0.000000000000000000, 0.000000000000000000, -9.974600000000000577 ) ) ;
#7049=FACE_OUTER_BOUND ( 'NONE', #1110, .T. ) ;
#7053=CARTESIAN_POINT ( 'NONE',  ( 2.459698528280935825, -7.240146430416073642, -0.09933465333851955459 ) ) ;
#7056=CARTESIAN_POINT ( 'NONE',  ( -7.500000000000000888, -1.443375672974068769, -7.063244554130002406 ) ) ;
#7063=DIRECTION ( 'NONE',  ( -0.5000000000000008882, -0.8660254037844382635, 0.000000000000000000 ) ) ;
#7108=ORIENTED_EDGE ( 'NONE', *, *, #11631, .F. ) ;
#7112=DIRECTION ( 'NONE',  ( 0.000000000000000000, 0.000000000000000000, 1.000000000000000000 ) ) ;
#7123=CARTESIAN_POINT ( 'NONE',  ( 0.000000000000000000, 0.000000000000000000, 0.000000000000000000 ) ) ;
#7133=AXIS2_PLACEMENT_3D ( 'NONE', #19555, #6656, #9940 ) ;
#7161=DIRECTION ( 'NONE',  ( 0.000000000000000000, 0.000000000000000000, 1.000000000000000000 ) ) ;
#7183=ORIENTED_EDGE ( 'NONE', *, *, #6246, .T. ) ;
#7189=LINE ( 'NONE', #1749, #1860 ) ;
#7200=CARTESIAN_POINT ( 'NONE',  ( 4.419133455864432847, -6.108866147516184952, -7.026396753507086146 ) ) ;
#7246=CONICAL_SURFACE ( 'NONE', #14617, 5.000000000000001776, 0.9599310885968795892 ) ;
#7257=EDGE_CURVE ( 'NONE', #2744, #4336, #4711, .T. ) ;
#7274=( BOUNDED_SURFACE ( )  B_SPLINE_SURFACE ( 3, 2, ( 
 ( #2479, #22639, #20845 ),
 ( #4301, #3803, #7680 ),
 ( #9868, #16742, #22517 ),
 ( #17223, #15073, #673 ),
 ( #22279, #5754, #11452 ),
 ( #8050, #22407, #11228 ),
 ( #7803, #9384, #5867 ),
 ( #201, #15186, #13275 ) ),
 .UNSPECIFIED., .F., .F., .F. ) 
 B_SPLINE_SURFACE_WITH_KNOTS ( ( 4, 2, 2, 4 ),
 ( 3, 3 ),
 ( 0.03851319102641418551, 0.04314724750133520914, 0.04546427573879571749, 0.04778130397625623277 ),
 ( 0.000000000000000000, 1.000000000000000000 ),
 .UNSPECIFIED. ) 
 GEOMETRIC_REPRESENTATION_ITEM ( )  RATIONAL_B_SPLINE_SURFACE ( (
 ( 1.000000000000000000, 0.8047781573724569482, 1.000000000000000000),
 ( 1.000000000000000000, 0.8123768202405010630, 1.000000000000000000),
 ( 1.000000000000000000, 0.8190667609311549358, 1.000000000000000000),
 ( 1.000000000000000000, 0.8191933927154739781, 1.000000000000000000),
 ( 1.000000000000000000, 0.8176088169850088683, 1.000000000000000000),
 ( 1.000000000000000000, 0.8122958474542694152, 1.000000000000000000),
 ( 1.000000000000000000, 0.8086309703845098174, 1.000000000000000000),
 ( 1.000000000000000000, 0.8047712409910821041, 1.000000000000000000) ) ) 
 REPRESENTATION_ITEM ( '' )  SURFACE ( )  );
#7280=CARTESIAN_POINT ( 'NONE',  ( 4.250000000000000000, 0.000000000000000000, -10.00000000000000000 ) ) ;
#7295=B_SPLINE_CURVE_WITH_KNOTS ( 'NONE', 3,
 ( #21015, #20522, #4474, #22697, #17405, #6171, #9922, #11879, #7856, #19187 ),
 .UNSPECIFIED., .F., .F.,
 ( 4, 2, 2, 2, 4 ),
 ( 0.000000000000000000, 0.002305503304226490767, 0.004611006608452981534, 0.006916509912679473168, 0.009222013216905964803 ),
 .UNSPECIFIED. ) ;
#7307=DIRECTION ( 'NONE',  ( 1.000000000000000000, 0.000000000000000000, 0.000000000000000000 ) ) ;
#7320=CARTESIAN_POINT ( 'NONE',  ( -5.007715329123872641E-16, -8.660254037844399733, -7.422398894150038728 ) ) ;
#7325=EDGE_LOOP ( 'NONE', ( #13993, #18651, #14101, #21159, #8342 ) ) ;
#7332=ORIENTED_EDGE ( 'NONE', *, *, #9354, .F. ) ;
#7334=AXIS2_PLACEMENT_3D ( 'NONE', #4775, #12186, #16015 ) ;
#7359=CARTESIAN_POINT ( 'NONE',  ( -7.848314987057850800, 4.129027267381560229, -7.493854785173809319 ) ) ;
#7388=CARTESIAN_POINT ( 'NONE',  ( -6.127431526422343306E-17, 9.147862274876549904, -8.047472243342932430 ) ) ;
#7395=CARTESIAN_POINT ( 'NONE',  ( 0.000000000000000000, 0.000000000000000000, -10.00000000000000000 ) ) ;
#7408=DIRECTION ( 'NONE',  ( -0.000000000000000000, -0.000000000000000000, 1.000000000000000000 ) ) ;
#7416=CARTESIAN_POINT ( 'NONE',  ( 6.874999999999997335, -4.690970937165716670, -7.298562697733105509 ) ) ;
#7421=CARTESIAN_POINT ( 'NONE',  ( 7.500000000000000888, 1.489914625144004523, -0.1187923833806749097 ) ) ;
#7445=CARTESIAN_POINT ( 'NONE',  ( -0.04606493828583551470, -9.175055303659563677, -8.057411785091794343 ) ) ;
#7448=EDGE_LOOP ( 'NONE', ( #8208, #22647 ) ) ;
#7463=CIRCLE ( 'NONE', #15963, 10.39117206796836079 ) ;
#7489=CARTESIAN_POINT ( 'NONE',  ( -7.500000000000000888, -0.7512838658081441023, 1.307818870560639724E-15 ) ) ;
#7533=CARTESIAN_POINT ( 'NONE',  ( 7.500000000000000000, 2.886751345948125547, -7.198902722707427593 ) ) ;
#7544=B_SPLINE_CURVE_WITH_KNOTS ( 'NONE', 3,
 ( #21254, #15944, #4705, #12115, #23284, #20138 ),
 .UNSPECIFIED., .F., .F.,
 ( 4, 2, 4 ),
 ( 0.000000000000000000, 0.002307655110370376069, 0.004615310220740751271 ),
 .UNSPECIFIED. ) ;
#7552=CARTESIAN_POINT ( 'NONE',  ( -7.500000000000000000, -4.330127018922198090, -7.422398894150034288 ) ) ;
#7557=VERTEX_POINT ( 'NONE', #22431 ) ;
#7591=CARTESIAN_POINT ( 'NONE',  ( -7.500000000000000000, -4.330127018922199866, -1.000000000000000888 ) ) ;
#7602=CARTESIAN_POINT ( 'NONE',  ( -3.280815508853482498, -7.221948645665452915, -7.591546097228404122 ) ) ;
#7616=EDGE_LOOP ( 'NONE', ( #20, #14324, #19764, #5532 ) ) ;
#7628=EDGE_CURVE ( 'NONE', #19884, #14233, #9411, .T. ) ;
#7652=EDGE_CURVE ( 'NONE', #14389, #14374, #21717, .T. ) ;
#7668=CARTESIAN_POINT ( 'NONE',  ( -5.000000000000000888, 6.123233995736767268E-16, -25.03750572909317285 ) ) ;
#7674=DIRECTION ( 'NONE',  ( 0.000000000000000000, 0.000000000000000000, 1.000000000000000000 ) ) ;
#7680=CARTESIAN_POINT ( 'NONE',  ( -7.908228835406498902, 3.123118350879302341, -7.776694659841278501 ) ) ;
#7748=CARTESIAN_POINT ( 'NONE',  ( 0.000000000000000000, 0.000000000000000000, -10.00000000000000000 ) ) ;
#7753=CARTESIAN_POINT ( 'NONE',  ( -0.3875187462251565851, -8.436519985395204202, -7.781689322724289148 ) ) ;
#7762=CARTESIAN_POINT ( 'NONE',  ( 0.000000000000000000, 0.000000000000000000, -10.00000000000000000 ) ) ;
#7803=CARTESIAN_POINT ( 'NONE',  ( -7.500000000000000000, -3.948305025207388130, -7.349903712356284480 ) ) ;
#7821=B_SPLINE_CURVE_WITH_KNOTS ( 'NONE', 3,
 ( #12945, #3833, #14850, #18441, #10895, #18327 ),
 .UNSPECIFIED., .F., .F.,
 ( 4, 2, 4 ),
 ( 0.000000000000000000, 0.002307655110370371299, 0.004615310220740742597 ),
 .UNSPECIFIED. ) ;
#7849=VERTEX_POINT ( 'NONE', #18900 ) ;
#7855=LINE ( 'NONE', #15238, #18428 ) ;
#7856=CARTESIAN_POINT ( 'NONE',  ( 0.6511518506208960888, -8.763486134561278007, -7.907570769506051533 ) ) ;
#7857=CARTESIAN_POINT ( 'NONE',  ( 10.12668159690567649, 0.000000000000000000, -9.999999999999998224 ) ) ;
#7874=ADVANCED_FACE ( 'NONE', ( #2231 ), #7274, .F. ) ;
#7899=DIRECTION ( 'NONE',  ( -0.000000000000000000, -0.000000000000000000, 1.000000000000000000 ) ) ;
#7936=AXIS2_PLACEMENT_3D ( 'NONE', #6092, #17211, #4288 ) ;
#7965=B_SPLINE_CURVE_WITH_KNOTS ( 'NONE', 3,
 ( #13142, #425, #2087, #13616, #6208, #2449 ),
 .UNSPECIFIED., .F., .F.,
 ( 4, 2, 4 ),
 ( -5.145455527293010977E-06, 0.0004153350442917342006, 0.0008358155441107593302 ),
 .UNSPECIFIED. ) ;
#7982=CARTESIAN_POINT ( 'NONE',  ( -6.523606932383669843, -4.893847819345372940, -7.213065638944913260 ) ) ;
#7993=CARTESIAN_POINT ( 'NONE',  ( 7.500000000000000000, 4.330127018922199866, -1.000000000000000888 ) ) ;
#7994=DIRECTION ( 'NONE',  ( -1.000000000000000000, 0.000000000000000000, 0.000000000000000000 ) ) ;
#7995=ORIENTED_EDGE ( 'NONE', *, *, #20321, .F. ) ;
#8009=CARTESIAN_POINT ( 'NONE',  ( -10.39117206796836079, 0.000000000000000000, -8.499999999999998224 ) ) ;
#8022=CIRCLE ( 'NONE', #19562, 4.250000000000000000 ) ;
#8050=CARTESIAN_POINT ( 'NONE',  ( -7.500000000000000000, -3.160302461882432024, -7.231849989190475725 ) ) ;
#8061=AXIS2_PLACEMENT_3D ( 'NONE', #2386, #20605, #8076 ) ;
#8076=DIRECTION ( 'NONE',  ( -1.000000000000000000, 0.000000000000000000, 0.000000000000000000 ) ) ;
#8090=AXIS2_PLACEMENT_3D ( 'NONE', #12181, #2938, #17681 ) ;
#8114=EDGE_CURVE ( 'NONE', #6861, #14389, #16720, .T. ) ;
#8135=VERTEX_POINT ( 'NONE', #18593 ) ;
#8136=B_SPLINE_CURVE_WITH_KNOTS ( 'NONE', 3,
 ( #11874, #18073, #8919, #14820, #1529, #3558 ),
 .UNSPECIFIED., .F., .F.,
 ( 4, 2, 4 ),
 ( 2.475503369207376426E-07, 0.002222330217055627170, 0.004444412883774334112 ),
 .UNSPECIFIED. ) ;
#8148=CARTESIAN_POINT ( 'NONE',  ( 7.915340744421234476, 3.857466640755322640, -7.913699667209310284 ) ) ;
#8151=EDGE_CURVE ( 'NONE', #8135, #23656, #3979, .T. ) ;
#8208=ORIENTED_EDGE ( 'NONE', *, *, #20877, .F. ) ;
#8217=FACE_OUTER_BOUND ( 'NONE', #21040, .T. ) ;
#8218=ORIENTED_EDGE ( 'NONE', *, *, #9100, .T. ) ;
#8233=CARTESIAN_POINT ( 'NONE',  ( 7.500000000000000000, -5.637851296924623057E-15, -6.991905250253753756 ) ) ;
#8246=CARTESIAN_POINT ( 'NONE',  ( -7.922281120364393914, 4.573931137438271399, -8.047472243342930653 ) ) ;
#8256=CARTESIAN_POINT ( 'NONE',  ( 7.500000000000000888, -4.651016565836964212, -7.928861822685564498 ) ) ;
#8261=CARTESIAN_POINT ( 'NONE',  ( 7.500000000000000888, -3.640541674360523228, -0.7158139487964624292 ) ) ;
#8300=CARTESIAN_POINT ( 'NONE',  ( -10.39117206796836257, 1.272551561242683764E-15, -8.499999999999998224 ) ) ;
#8312=ADVANCED_FACE ( 'NONE', ( #2301 ), #3252, .F. ) ;
#8342=ORIENTED_EDGE ( 'NONE', *, *, #23734, .T. ) ;
#8351=CARTESIAN_POINT ( 'NONE',  ( 0.000000000000000000, 0.000000000000000000, 0.000000000000000000 ) ) ;
#8368=CARTESIAN_POINT ( 'NONE',  ( 7.499999999999999112, 3.105728215500122680, -7.659336188854854122 ) ) ;
#8433=CARTESIAN_POINT ( 'NONE',  ( -7.297096662748653293E-16, -8.716842316802402735, -7.700127545397317697 ) ) ;
#8435=PRODUCT_DEFINITION_SHAPE ( 'NONE', 'NONE',  #16109 ) ;
#8458=CIRCLE ( 'NONE', #10000, 5.000000000000001776 ) ;
#8514=ORIENTED_EDGE ( 'NONE', *, *, #20180, .T. ) ;
#8578=FACE_OUTER_BOUND ( 'NONE', #16444, .T. ) ;
#8580=CARTESIAN_POINT ( 'NONE',  ( -4.419133455862249704, 6.108866147517435508, -7.026396753507433424 ) ) ;
#8592=CARTESIAN_POINT ( 'NONE',  ( 5.335963852943280017, 6.035591050531201596, -7.593821156097048330 ) ) ;
#8612=CARTESIAN_POINT ( 'NONE',  ( 7.500000000000000000, 3.948247735265829395, -7.349893093595813554 ) ) ;
#8699=CARTESIAN_POINT ( 'NONE',  ( -5.088535779737005882, 5.722386535631696525, -7.491772860716161553 ) ) ;
#8712=CARTESIAN_POINT ( 'NONE',  ( 7.777900015783946408, 4.169681370001526055, -7.928862157988300297 ) ) ;
#8717=DIRECTION ( 'NONE',  ( -1.000000000000000000, 0.000000000000000000, 0.000000000000000000 ) ) ;
#8767=CARTESIAN_POINT ( 'NONE',  ( 0.000000000000000000, 0.000000000000000000, -25.03750572909317285 ) ) ;
#8786=VECTOR ( 'NONE', #5635, 1000.000000000000000 ) ;
#8819=CARTESIAN_POINT ( 'NONE',  ( 0.000000000000000000, 0.000000000000000000, -9.226681596905677907 ) ) ;
#8843=EDGE_CURVE ( 'NONE', #12980, #9344, #5278, .T. ) ;
#8859=STYLED_ITEM ( 'NONE', ( #12184 ), #17647 ) ;
#8917=( NAMED_UNIT ( * ) SI_UNIT ( $, .STERADIAN. ) SOLID_ANGLE_UNIT ( ) );
#8919=CARTESIAN_POINT ( 'NONE',  ( -6.293430271071534854, 5.026740376715094882, -0.4524126574264483169 ) ) ;
#8951=CARTESIAN_POINT ( 'NONE',  ( -0.9763930676156993282, 8.096533237421580154, -7.213065638943424673 ) ) ;
#8966=CARTESIAN_POINT ( 'NONE',  ( -0.5974722283283655511, 8.315303285985683246, -0.7026937717022859742 ) ) ;
#8999=FILL_AREA_STYLE ('',( #23361 ) ) ;
#9000=CYLINDRICAL_SURFACE ( 'NONE', #2220, 5.000000000000000888 ) ;
#9001=CARTESIAN_POINT ( 'NONE',  ( 7.914984360234579519, -3.818534719232097974, -7.907701344400643428 ) ) ;
#9020=CARTESIAN_POINT ( 'NONE',  ( 7.500000000000000000, -4.330127018922199866, -10.00000000000000000 ) ) ;
#9036=CARTESIAN_POINT ( 'NONE',  ( 2.325424218458714165, -7.317669739337183898, -7.030005583191490715 ) ) ;
#9063=DIRECTION ( 'NONE',  ( -1.000000000000000000, 0.000000000000000000, 0.000000000000000000 ) ) ;
#9065=ORIENTED_EDGE ( 'NONE', *, *, #20321, .T. ) ;
#9073=ORIENTED_EDGE ( 'NONE', *, *, #12155, .T. ) ;
#9094=CYLINDRICAL_SURFACE ( 'NONE', #9165, 4.250000000000000000 ) ;
#9100=EDGE_CURVE ( 'NONE', #23060, #2744, #11523, .T. ) ;
#9118=CARTESIAN_POINT ( 'NONE',  ( -7.500000000000000888, 3.639598441879742907, -0.7155132341745253921 ) ) ;
#9165=AXIS2_PLACEMENT_3D ( 'NONE', #7395, #11173, #10819 ) ;
#9202=CARTESIAN_POINT ( 'NONE',  ( -1.211595439868048629, 7.960739084487649109, -0.4504974108211966533 ) ) ;
#9210=VERTEX_POINT ( 'NONE', #17569 ) ;
#9234=CARTESIAN_POINT ( 'NONE',  ( 0.000000000000000000, 0.000000000000000000, -9.974600000000000577 ) ) ;
#9246=CARTESIAN_POINT ( 'NONE',  ( -7.500000000000000000, 3.608439182435158710, -7.298562697733104621 ) ) ;
#9252=CARTESIAN_POINT ( 'NONE',  ( 7.500000000000000888, -2.886751345948134873, -7.198902722707428481 ) ) ;
#9266=ORIENTED_EDGE ( 'NONE', *, *, #18137, .F. ) ;
#9292=ADVANCED_FACE ( 'NONE', ( #1385 ), #9000, .F. ) ;
#9333=CARTESIAN_POINT ( 'NONE',  ( 0.000000000000000000, 0.000000000000000000, -9.999999999999998224 ) ) ;
#9344=VERTEX_POINT ( 'NONE', #18173 ) ;
#9354=EDGE_CURVE ( 'NONE', #18546, #12980, #20403, .T. ) ;
#9381=EDGE_CURVE ( 'NONE', #21582, #6258, #13821, .T. ) ;
#9384=CARTESIAN_POINT ( 'NONE',  ( -7.500000000000000000, -3.882691789160215290, -7.781695678273567118 ) ) ;
#9411=B_SPLINE_CURVE_WITH_KNOTS ( 'NONE', 3,
 ( #21459, #17382, #17722, #12213, #19395, #21103 ),
 .UNSPECIFIED., .F., .F.,
 ( 4, 2, 4 ),
 ( 2.475503369438313607E-07, 0.002222330217055647119, 0.004444412883774350592 ),
 .UNSPECIFIED. ) ;
#9423=CARTESIAN_POINT ( 'NONE',  ( 0.6169862416622686752, 8.783631307150953305, -7.913704048099833521 ) ) ;
#9431=CARTESIAN_POINT ( 'NONE',  ( -1.306442393143578462, -8.377108146505394259, -7.792327460285862983 ) ) ;
#9434=DIRECTION ( 'NONE',  ( 0.9396926207859143121, 1.150791560227857665E-16, -0.3420201433256525592 ) ) ;
#9440=EDGE_CURVE ( 'NONE', #4056, #12980, #7965, .T. ) ;
#9473=CARTESIAN_POINT ( 'NONE',  ( 0.000000000000000000, 0.000000000000000000, 0.000000000000000000 ) ) ;
#9517=CARTESIAN_POINT ( 'NONE',  ( 6.602753909532903087, 5.319290460493537154, -7.792447862505332168 ) ) ;
#9519=ORIENTED_EDGE ( 'NONE', *, *, #7652, .F. ) ;
#9554=ORIENTED_EDGE ( 'NONE', *, *, #17713, .T. ) ;
#9571=EDGE_CURVE ( 'NONE', #1621, #18546, #19500, .T. ) ;
#9590=ORIENTED_EDGE ( 'NONE', *, *, #12294, .F. ) ;
#9616=ADVANCED_FACE ( 'NONE', ( #986 ), #23774, .F. ) ;
#9624=CARTESIAN_POINT ( 'NONE',  ( 0.000000000000000000, 0.000000000000000000, -9.999999999999998224 ) ) ;
#9711=DIRECTION ( 'NONE',  ( 1.000000000000000000, 0.000000000000000000, 0.000000000000000000 ) ) ;
#9749=DIRECTION ( 'NONE',  ( 1.000000000000000000, 0.000000000000000000, 0.000000000000000000 ) ) ;
#9751=ORIENTED_EDGE ( 'NONE', *, *, #999, .T. ) ;
#9806=CARTESIAN_POINT ( 'NONE',  ( 0.3483149870578491347, -8.861353789385031376, -7.493854785173814648 ) ) ;
#9811=VERTEX_POINT ( 'NONE', #7388 ) ;
#9817=CARTESIAN_POINT ( 'NONE',  ( 7.500000000000000888, 3.639598441879751345, -0.7155132341745285007 ) ) ;
#9818=DIRECTION ( 'NONE',  ( 1.000000000000000000, 0.000000000000000000, 0.000000000000000000 ) ) ;
#9829=CARTESIAN_POINT ( 'NONE',  ( 0.6250000000000013323, 8.299410119600871383, -7.298562697733108173 ) ) ;
#9868=CARTESIAN_POINT ( 'NONE',  ( -7.500000000000000000, 1.644753667986373458, -7.029983668655349405 ) ) ;
#9914=DIRECTION ( 'NONE',  ( 0.000000000000000000, 0.000000000000000000, 1.000000000000000000 ) ) ;
#9916=ORIENTED_EDGE ( 'NONE', *, *, #1150, .T. ) ;
#9922=CARTESIAN_POINT ( 'NONE',  ( 2.623433461001182909, -7.604994000793866782, -7.633824513837117465 ) ) ;
#9927=CARTESIAN_POINT ( 'NONE',  ( -0.3306966981848578069, -8.469326210127253063, -7.349897473154448413 ) ) ;
#9940=DIRECTION ( 'NONE',  ( 1.000000000000000000, 0.000000000000000000, 0.000000000000000000 ) ) ;
#9979=CARTESIAN_POINT ( 'NONE',  ( 4.403473400622098133, 6.117907484625861869, 2.043043468777371629E-15 ) ) ;
#9991=VECTOR ( 'NONE', #21436, 1000.000000000000114 ) ;
#9992=ORIENTED_EDGE ( 'NONE', *, *, #12991, .F. ) ;
#10000=AXIS2_PLACEMENT_3D ( 'NONE', #7048, #7408, #6940 ) ;
#10038=ORIENTED_EDGE ( 'NONE', *, *, #3626, .F. ) ;
#10059=CARTESIAN_POINT ( 'NONE',  ( -1.282512619719133662, -8.391164935524759727, -7.795653906409117262 ) ) ;
#10075=ORIENTED_EDGE ( 'NONE', *, *, #9571, .F. ) ;
#10093=CARTESIAN_POINT ( 'NONE',  ( 7.894958282449824338, -1.603399432398892266, -7.593838100136980351 ) ) ;
#10147=CARTESIAN_POINT ( 'NONE',  ( 10.12668159690567649, 0.000000000000000000, -9.226681596905677907 ) ) ;
#10159=CARTESIAN_POINT ( 'NONE',  ( 4.336808689942017736E-16, 8.660254037844390851, -1.000000000000000888 ) ) ;
#10160=CARTESIAN_POINT ( 'NONE',  ( 0.000000000000000000, 0.000000000000000000, -25.03750572909317285 ) ) ;
#10206=ORIENTED_EDGE ( 'NONE', *, *, #12128, .T. ) ;
#10214=CARTESIAN_POINT ( 'NONE',  ( 6.288404560131952259, 5.029641972278931839, -0.4504974108211943773 ) ) ;
#10305=ORIENTED_EDGE ( 'NONE', *, *, #11441, .F. ) ;
#10340=CARTESIAN_POINT ( 'NONE',  ( 0.5974722283283632196, -8.315303285985693904, -0.7026937717022971874 ) ) ;
#10413=CARTESIAN_POINT ( 'NONE',  ( -2.325424218463065351, 7.317669739334662360, -7.030005583190789054 ) ) ;
#10425=CARTESIAN_POINT ( 'NONE',  ( 6.658902113225075858, 5.287118297641098863, -7.776713651267108673 ) ) ;
#10453=CARTESIAN_POINT ( 'NONE',  ( 7.500000000000000000, 0.7723602884954153813, -7.026388801733942202 ) ) ;
#10469=LINE ( 'NONE', #4653, #23108 ) ;
#10541=B_SPLINE_CURVE_WITH_KNOTS ( 'NONE', 3,
 ( #6671, #14065, #3386, #16330, #23321, #5922, #7489, #13099 ),
 .UNSPECIFIED., .F., .F.,
 ( 4, 2, 2, 4 ),
 ( 0.006061689441712453386, 0.007174127271521677299, 0.008286565101330901212, 0.01051144076094934904 ),
 .UNSPECIFIED. ) ;
#10551=B_SPLINE_CURVE_WITH_KNOTS ( 'NONE', 3,
 ( #17676, #4885, #10586, #12072, #19601, #4659 ),
 .UNSPECIFIED., .F., .F.,
 ( 4, 2, 4 ),
 ( 0.004615310220740751271, 0.006918661718823357169, 0.009222013216905963068 ),
 .UNSPECIFIED. ) ;
#10572=CARTESIAN_POINT ( 'NONE',  ( 7.500000000000000000, -2.571118828324946648, -0.3627527587569098766 ) ) ;
#10584=DIRECTION ( 'NONE',  ( -1.000000000000000000, 0.000000000000000000, 0.000000000000000000 ) ) ;
#10586=CARTESIAN_POINT ( 'NONE',  ( -7.897850199329715437, 1.533397866934075759, -7.634054012537968781 ) ) ;
#10688=AXIS2_PLACEMENT_3D ( 'NONE', #12797, #7063, #14451 ) ;
#10698=( BOUNDED_SURFACE ( )  B_SPLINE_SURFACE ( 3, 2, ( 
 ( #18203, #95, #7445 ),
 ( #20005, #18422, #12927 ),
 ( #9036, #3688, #19890 ),
 ( #7200, #20239, #16395 ),
 ( #22166, #16748, #23746 ),
 ( #14589, #5640, #13048 ),
 ( #16508, #3342, #1881 ),
 ( #20350, #3813, #11102 ) ),
 .UNSPECIFIED., .F., .F., .F. ) 
 B_SPLINE_SURFACE_WITH_KNOTS ( ( 4, 2, 2, 4 ),
 ( 3, 3 ),
 ( 0.03861844051980971304, 0.04325213341840643266, 0.04556897986770479247, 0.04788582631700314535 ),
 ( 0.000000000000000000, 1.000000000000000000 ),
 .UNSPECIFIED. ) 
 GEOMETRIC_REPRESENTATION_ITEM ( )  RATIONAL_B_SPLINE_SURFACE ( (
 ( 1.000000000000000000, 0.8047781759831919013, 1.000000000000000000),
 ( 1.000000000000000000, 0.8123762462802479600, 1.000000000000000000),
 ( 1.000000000000000000, 0.8190659850620179983, 1.000000000000000000),
 ( 1.000000000000000000, 0.8191937571011910224, 1.000000000000000000),
 ( 1.000000000000000000, 0.8176092952781196521, 1.000000000000000000),
 ( 1.000000000000000000, 0.8122962088595743202, 1.000000000000000000),
 ( 1.000000000000000000, 0.8086311330828506172, 1.000000000000000000),
 ( 1.000000000000000000, 0.8047712282214323221, 1.000000000000000000) ) ) 
 REPRESENTATION_ITEM ( '' )  SURFACE ( )  );
#10700=CARTESIAN_POINT ( 'NONE',  ( -7.640563834021360018E-16, -9.147862274876560562, -8.047472243342937759 ) ) ;
#10710=EDGE_CURVE ( 'NONE', #21875, #306, #23214, .T. ) ;
#10715=CARTESIAN_POINT ( 'NONE',  ( 6.250000000000000000, -5.051814855409237026, -7.198902722707430257 ) ) ;
#10732=CARTESIAN_POINT ( 'NONE',  ( -7.894787914004607998, -1.230850257101226302E-13, -7.591390474663425536 ) ) ;
#10763=EDGE_CURVE ( 'NONE', #17922, #6350, #13138, .T. ) ;
#10767=FACE_OUTER_BOUND ( 'NONE', #14271, .T. ) ;
#10772=AXIS2_PLACEMENT_3D ( 'NONE', #14578, #22045, #20226 ) ;
#10794=CARTESIAN_POINT ( 'NONE',  ( 7.500000000000007105, -4.330127018922196314, -7.564338275809341816 ) ) ;
#10819=DIRECTION ( 'NONE',  ( 1.000000000000000000, 0.000000000000000000, 0.000000000000000000 ) ) ;
#10822=LINE ( 'NONE', #5114, #13115 ) ;
#10827=ORIENTED_EDGE ( 'NONE', *, *, #7628, .F. ) ;
#10852=AXIS2_PLACEMENT_3D ( 'NONE', #23290, #17503, #15711 ) ;
#10895=CARTESIAN_POINT ( 'NONE',  ( 7.894787914004607998, 0.7661396099416312166, -7.591390474663430865 ) ) ;
#10905=EDGE_CURVE ( 'NONE', #16143, #9210, #7295, .T. ) ;
#10927=ORIENTED_EDGE ( 'NONE', *, *, #22537, .F. ) ;
#10997=CARTESIAN_POINT ( 'NONE',  ( 7.922281120364393914, 4.573931137438269623, -8.047472243342930653 ) ) ;
#11004=ORIENTED_EDGE ( 'NONE', *, *, #2382, .T. ) ;
#11021=CARTESIAN_POINT ( 'NONE',  ( -2.352990130084580066E-16, 8.660254037844390851, -7.422398894150034288 ) ) ;
#11056=VERTEX_POINT ( 'NONE', #22760 ) ;
#11068=CARTESIAN_POINT ( 'NONE',  ( 7.894787914004607998, 1.243647571710251278E-13, -7.591390474663425536 ) ) ;
#11087=CARTESIAN_POINT ( 'NONE',  ( -0.6249999999999991118, -8.299410119600880265, -7.298562697733108173 ) ) ;
#11093=APPLICATION_CONTEXT ( 'automotive_design' ) ;
#11095=ORIENTED_EDGE ( 'NONE', *, *, #7628, .T. ) ;
#11102=CARTESIAN_POINT ( 'NONE',  ( 7.970070017554212960, -4.546953124339766283, -8.057670357645358550 ) ) ;
#11110=CARTESIAN_POINT ( 'NONE',  ( 1.306442393143578906, 8.377108146505383601, -7.792327460285857654 ) ) ;
#11114=ORIENTED_EDGE ( 'NONE', *, *, #10763, .T. ) ;
#11147=CARTESIAN_POINT ( 'NONE',  ( -2.621086668468698644, -7.606368536631371136, -7.634085501268427443 ) ) ;
#11154=CARTESIAN_POINT ( 'NONE',  ( 4.336808689942017736E-16, 8.660254037844390851, -1.000000000000000888 ) ) ;
#11159=CARTESIAN_POINT ( 'NONE',  ( -4.250000000000000000, 5.204748896376250699E-16, -10.00000000000000000 ) ) ;
#11173=DIRECTION ( 'NONE',  ( 0.000000000000000000, 0.000000000000000000, 1.000000000000000000 ) ) ;
#11174=VECTOR ( 'NONE', #15387, 1000.000000000000000 ) ;
#11190=( GEOMETRIC_REPRESENTATION_CONTEXT ( 3 ) GLOBAL_UNCERTAINTY_ASSIGNED_CONTEXT ( ( #20618 ) ) GLOBAL_UNIT_ASSIGNED_CONTEXT ( ( #23236, #5025, #21558 ) ) REPRESENTATION_CONTEXT ( 'NONE', 'WORKASPACE' ) );
#11210=AXIS2_PLACEMENT_3D ( 'NONE', #9473, #14914, #3769 ) ;
#11228=CARTESIAN_POINT ( 'NONE',  ( -7.908219015560238319, -3.084967917785936820, -7.795665562178438535 ) ) ;
#11256=CARTESIAN_POINT ( 'NONE',  ( -6.486836893983275232, 4.915077010913945443, -7.231838333420560261 ) ) ;
#11273=CARTESIAN_POINT ( 'NONE',  ( -7.922281120364393914, -4.573931137438277617, -8.047472243342932430 ) ) ;
#11321=DIRECTION ( 'NONE',  ( -0.000000000000000000, -0.000000000000000000, 1.000000000000000000 ) ) ;
#11338=CARTESIAN_POINT ( 'NONE',  ( 0.000000000000000000, 0.000000000000000000, -10.00000000000000000 ) ) ;
#11354=ORIENTED_EDGE ( 'NONE', *, *, #12630, .F. ) ;
#11356=SHAPE_DEFINITION_REPRESENTATION ( #8435, #22995 ) ;
#11357=CARTESIAN_POINT ( 'NONE',  ( 7.922281120364393914, 4.573931137438269623, -8.047472243342930653 ) ) ;
#11441=EDGE_CURVE ( 'NONE', #14374, #5614, #7463, .T. ) ;
#11452=CARTESIAN_POINT ( 'NONE',  ( -7.897827455343210623, -1.533134349199909208, -7.633632140068262295 ) ) ;
#11479=CARTESIAN_POINT ( 'NONE',  ( -7.112481253775184697, 4.553861071372892866, -7.781689322728085223 ) ) ;
#11501=ADVANCED_FACE ( 'NONE', ( #2767, #8217 ), #2526, .T. ) ;
#11506=DIRECTION ( 'NONE',  ( 0.000000000000000000, 0.000000000000000000, -1.000000000000000000 ) ) ;
#11523=CIRCLE ( 'NONE', #307, 5.000000000000000888 ) ;
#11604=B_SPLINE_CURVE_WITH_KNOTS ( 'NONE', 3,
 ( #1795, #20154, #21975, #5549, #3601, #11021 ),
 .UNSPECIFIED., .F., .F.,
 ( 4, 2, 4 ),
 ( -5.145455527296316946E-06, 0.0004153350442917303517, 0.0008358155441107569450 ),
 .UNSPECIFIED. ) ;
#11630=CARTESIAN_POINT ( 'NONE',  ( -5.040301471719076609, -5.750234626350520628, -0.09933465333851741741 ) ) ;
#11631=EDGE_CURVE ( 'NONE', #4056, #19785, #7544, .T. ) ;
#11651=CARTESIAN_POINT ( 'NONE',  ( -2.411464220262952818, -7.267994521134228059, -7.491772860715828486 ) ) ;
#11668=CARTESIAN_POINT ( 'NONE',  ( 6.874999999999999112, 4.690970937165706900, -7.298562697733104621 ) ) ;
#11700=EDGE_CURVE ( 'NONE', #23656, #19450, #17861, .T. ) ;
#11762=CARTESIAN_POINT ( 'NONE',  ( -6.658902113226115027, -5.287118297636088649, -7.776713651266535798 ) ) ;
#11767=ORIENTED_EDGE ( 'NONE', *, *, #20225, .T. ) ;
#11784=CIRCLE ( 'NONE', #3618, 4.250000000000000000 ) ;
#11799=FACE_OUTER_BOUND ( 'NONE', #7325, .T. ) ;
#11844=CIRCLE ( 'NONE', #14143, 7.500000000000001776 ) ;
#11874=CARTESIAN_POINT ( 'NONE',  ( -7.500000000000000000, 4.330127018922191873, -0.9999999999999970024 ) ) ;
#11879=CARTESIAN_POINT ( 'NONE',  ( 1.305263714129178743, -8.377797850839291627, -7.792447862505339273 ) ) ;
#11881=ORIENTED_EDGE ( 'NONE', *, *, #6674, .F. ) ;
#11882=CARTESIAN_POINT ( 'NONE',  ( -5.174575781537456010, -5.672711317431625488, -7.030005583190790830 ) ) ;
#11914=CARTESIAN_POINT ( 'NONE',  ( 7.499999999999999112, 0.7577384720672989404, -7.446470314338469620 ) ) ;
#12014=AXIS2_PLACEMENT_3D ( 'NONE', #6256, #13189, #6006 ) ;
#12072=CARTESIAN_POINT ( 'NONE',  ( -7.908030677224553884, 3.059924800338342799, -7.792662696733364314 ) ) ;
#12095=ORIENTED_EDGE ( 'NONE', *, *, #8114, .T. ) ;
#12097=MANIFOLD_SOLID_BREP ( 'EndChamfer', #3644 ) ;
#12115=CARTESIAN_POINT ( 'NONE',  ( -7.897836333153808397, -1.530409084195006653, -7.633857274177628938 ) ) ;
#12128=EDGE_CURVE ( 'NONE', #23060, #5418, #22267, .T. ) ;
#12155=EDGE_CURVE ( 'NONE', #7557, #23656, #11784, .T. ) ;
#12176=PLANE ( 'NONE',  #21352 ) ;
#12181=CARTESIAN_POINT ( 'NONE',  ( 0.000000000000000000, 0.000000000000000000, -9.449444346342714240 ) ) ;
#12184=PRESENTATION_STYLE_ASSIGNMENT (( #4773 ) ) ;
#12186=DIRECTION ( 'NONE',  ( 0.5000000000000006661, 0.8660254037844383745, -0.000000000000000000 ) ) ;
#12196=CARTESIAN_POINT ( 'NONE',  ( 5.000000000000000888, 0.000000000000000000, 0.000000000000000000 ) ) ;
#12213=CARTESIAN_POINT ( 'NONE',  ( -2.452879891156814818, -7.244083172395189507, -0.1007566405101857632 ) ) ;
#12236=CYLINDRICAL_SURFACE ( 'NONE', #17383, 5.000000000000000888 ) ;
#12294=EDGE_CURVE ( 'NONE', #17922, #306, #22940, .T. ) ;
#12302=SHAPE_REPRESENTATION_RELATIONSHIP ( 'NONE' , 'NONE' ,  #22995, #17647 ) ;
#12335=CARTESIAN_POINT ( 'NONE',  ( -10.12668159690567649, 1.240160820363494356E-15, -9.226681596905677907 ) ) ;
#12368=CARTESIAN_POINT ( 'NONE',  ( -1.249327701954873415, 8.410337540189265937, -7.776713651267812999 ) ) ;
#12431=ADVANCED_FACE ( 'NONE', ( #12647 ), #12176, .T. ) ;
#12436=CARTESIAN_POINT ( 'NONE',  ( 7.500000000000000000, -4.330127018922199866, -7.422398894150035176 ) ) ;
#12499=CARTESIAN_POINT ( 'NONE',  ( 4.174999999999999822, 0.000000000000000000, -0.5776712190230133270 ) ) ;
#12513=ORIENTED_EDGE ( 'NONE', *, *, #8151, .T. ) ;
#12543=CARTESIAN_POINT ( 'NONE',  ( -7.500000000000000000, -4.330127018922198090, -7.422398894150034288 ) ) ;
#12553=FACE_BOUND ( 'NONE', #20692, .T. ) ;
#12561=( NAMED_UNIT ( * ) PLANE_ANGLE_UNIT ( ) SI_UNIT ( $, .RADIAN. ) );
#12600=ADVANCED_FACE ( 'NONE', ( #12620 ), #3970, .T. ) ;
#12620=FACE_OUTER_BOUND ( 'NONE', #17270, .T. ) ;
#12630=EDGE_CURVE ( 'NONE', #23462, #16143, #20047, .T. ) ;
#12642=ORIENTED_EDGE ( 'NONE', *, *, #18005, .F. ) ;
#12647=FACE_OUTER_BOUND ( 'NONE', #929, .T. ) ;
#12721=CONICAL_SURFACE ( 'NONE', #17664, 4.174999999999999822, 0.9599310885968795892 ) ;
#12729=CARTESIAN_POINT ( 'NONE',  ( 1.060314165522845187, 8.048081368953960535, -7.659344964963204383 ) ) ;
#12768=ORIENTED_EDGE ( 'NONE', *, *, #9100, .F. ) ;
#12793=CARTESIAN_POINT ( 'NONE',  ( -7.499999999999998224, 1.489914625143999416, -0.1187923833806747292 ) ) ;
#12797=CARTESIAN_POINT ( 'NONE',  ( -7.500000000000000000, -4.330127018922198090, -10.00000000000000000 ) ) ;
#12827=DIRECTION ( 'NONE',  ( 0.8660254037844382635, 0.5000000000000004441, 0.000000000000000000 ) ) ;
#12850=DIRECTION ( 'NONE',  ( 0.000000000000000000, 0.000000000000000000, 1.000000000000000000 ) ) ;
#12915=DIRECTION ( 'NONE',  ( 1.000000000000000000, 0.000000000000000000, 0.000000000000000000 ) ) ;
#12927=CARTESIAN_POINT ( 'NONE',  ( 1.249327701954825010, -8.410337540182549532, -7.776713651265369620 ) ) ;
#12936=ORIENTED_EDGE ( 'NONE', *, *, #11700, .T. ) ;
#12941=CARTESIAN_POINT ( 'NONE',  ( 7.500000000000000000, 4.330127018922190096, -7.422398894150032511 ) ) ;
#12945=CARTESIAN_POINT ( 'NONE',  ( 7.922281120364393914, 4.573931137438269623, -8.047472243342930653 ) ) ;
#12948=CARTESIAN_POINT ( 'NONE',  ( 0.000000000000000000, 0.000000000000000000, 0.000000000000000000 ) ) ;
#12980=VERTEX_POINT ( 'NONE', #7552 ) ;
#12982=TOROIDAL_SURFACE ( 'NONE', #3243, 10.12668159690567649, 0.7733184030943209830 ) ;
#12991=EDGE_CURVE ( 'NONE', #14389, #6861, #15600, .T. ) ;
#12998=ORIENTED_EDGE ( 'NONE', *, *, #5892, .T. ) ;
#13010=CARTESIAN_POINT ( 'NONE',  ( -7.500000000000000888, 2.575910028905295857, -0.3641256808890092067 ) ) ;
#13017=CARTESIAN_POINT ( 'NONE',  ( 7.500000000000001776, 0.000000000000000000, 0.000000000000000000 ) ) ;
#13048=CARTESIAN_POINT ( 'NONE',  ( 6.625705691649528717, -5.306270977113132226, -7.795653906408932521 ) ) ;
#13071=VERTEX_POINT ( 'NONE', #15897 ) ;
#13082=CARTESIAN_POINT ( 'NONE',  ( -0.3483149870578547969, 8.861353789385022495, -7.493854785173811983 ) ) ;
#13087=CARTESIAN_POINT ( 'NONE',  ( -4.606548227981510202, -6.456511556909259930, -7.591235721156638583 ) ) ;
#13090=CONICAL_SURFACE ( 'NONE', #17299, 7.500000000000001776, 0.8594454914424796144 ) ;
#13099=CARTESIAN_POINT ( 'NONE',  ( -7.500000000000001776, 0.000000000000000000, 0.000000000000000000 ) ) ;
#13115=VECTOR ( 'NONE', #18158, 1000.000000000000000 ) ;
#13117=DIRECTION ( 'NONE',  ( -0.000000000000000000, -0.000000000000000000, -1.000000000000000000 ) ) ;
#13138=CIRCLE ( 'NONE', #2675, 7.500000000000001776 ) ;
#13142=CARTESIAN_POINT ( 'NONE',  ( -7.922281120364393914, -4.573931137438277617, -8.047472243342932430 ) ) ;
#13165=DIRECTION ( 'NONE',  ( -0.000000000000000000, -0.000000000000000000, 1.000000000000000000 ) ) ;
#13185=CARTESIAN_POINT ( 'NONE',  ( 0.6508621380849231031, 8.763657152406445050, -7.907633014911220393 ) ) ;
#13189=DIRECTION ( 'NONE',  ( 0.000000000000000000, 0.000000000000000000, -1.000000000000000000 ) ) ;
#13196=CARTESIAN_POINT ( 'NONE',  ( -6.625705691649848461, 5.306270977113102916, -7.795653906409009792 ) ) ;
#13233=ORIENTED_EDGE ( 'NONE', *, *, #20849, .F. ) ;
#13241=B_SPLINE_CURVE_WITH_KNOTS ( 'NONE', 3,
 ( #13311, #20622, #11630, #17029, #482, #7591 ),
 .UNSPECIFIED., .F., .F.,
 ( 4, 2, 4 ),
 ( 0.004444412883774350592, 0.006655097293744440673, 0.008865781703714530754 ),
 .UNSPECIFIED. ) ;
#13275=CARTESIAN_POINT ( 'NONE',  ( -7.922811899608408481, -4.628803996615321381, -8.057669882367649805 ) ) ;
#13291=CARTESIAN_POINT ( 'NONE',  ( 5.274401269815139237, 6.074457022762083547, -7.633824513837111247 ) ) ;
#13302=CARTESIAN_POINT ( 'NONE',  ( -7.970070017554212960, 4.546953124339755625, -8.057670357645356773 ) ) ;
#13311=CARTESIAN_POINT ( 'NONE',  ( -3.750000000000007105, -6.495190528383289141, 0.000000000000000000 ) ) ;
#13347=ORIENTED_EDGE ( 'NONE', *, *, #23734, .F. ) ;
#13483=CARTESIAN_POINT ( 'NONE',  ( 3.749999999999998224, 6.495190528383290918, -6.991905250253753756 ) ) ;
#13530=ORIENTED_EDGE ( 'NONE', *, *, #19048, .T. ) ;
#13549=DIRECTION ( 'NONE',  ( -0.000000000000000000, -0.000000000000000000, 1.000000000000000000 ) ) ;
#13579=DIRECTION ( 'NONE',  ( 1.000000000000000000, 0.000000000000000000, 0.000000000000000000 ) ) ;
#13616=CARTESIAN_POINT ( 'NONE',  ( -7.549004593702462351, -4.358419834287841965, -7.700121441565841884 ) ) ;
#13639=EDGE_CURVE ( 'NONE', #19785, #14374, #639, .T. ) ;
#13652=ORIENTED_EDGE ( 'NONE', *, *, #1199, .T. ) ;
#13679=AXIS2_PLACEMENT_3D ( 'NONE', #12335, #17483, #928 ) ;
#13732=CARTESIAN_POINT ( 'NONE',  ( 7.500000000000000000, 4.330127018922190096, -10.00000000000000000 ) ) ;
#13801=EDGE_CURVE ( 'NONE', #9344, #21582, #10541, .T. ) ;
#13811=CARTESIAN_POINT ( 'NONE',  ( -1.013163106016700565, -8.075304045852661261, -7.231838333420565590 ) ) ;
#13821=B_SPLINE_CURVE_WITH_KNOTS ( 'NONE', 3,
 ( #22130, #23600, #5373, #12793, #20097, #13010, #16609, #9118, #3542, #65 ),
 .UNSPECIFIED., .F., .F.,
 ( 4, 2, 2, 2, 4 ),
 ( 0.01051144076094934904, 0.01162027323572610918, 0.01272910571050286932, 0.01383793818527962946, 0.01494677066005638960 ),
 .UNSPECIFIED. ) ;
#13863=ORIENTED_EDGE ( 'NONE', *, *, #9381, .T. ) ;
#13922=ORIENTED_EDGE ( 'NONE', *, *, #16411, .F. ) ;
#13953=DIRECTION ( 'NONE',  ( 0.8191520442889907994, 0.000000000000000000, 0.5735764363510474917 ) ) ;
#13955=ORIENTED_EDGE ( 'NONE', *, *, #19153, .F. ) ;
#13960=CARTESIAN_POINT ( 'NONE',  ( 0.000000000000000000, 0.000000000000000000, -8.499999999999998224 ) ) ;
#13961=CARTESIAN_POINT ( 'NONE',  ( -1.305263714129178521, 8.377797850839286298, -7.792447862505335721 ) ) ;
#13993=ORIENTED_EDGE ( 'NONE', *, *, #14182, .F. ) ;
#13995=FACE_OUTER_BOUND ( 'NONE', #4747, .T. ) ;
#13997=ORIENTED_EDGE ( 'NONE', *, *, #5892, .F. ) ;
#14008=ORIENTED_EDGE ( 'NONE', *, *, #20616, .T. ) ;
#14051=CARTESIAN_POINT ( 'NONE',  ( 7.847095227763521308, 4.129731495738485414, -7.493596212620238894 ) ) ;
#14062=CARTESIAN_POINT ( 'NONE',  ( 7.808623696107882317, -4.508310992946666040, -7.999704684617485739 ) ) ;
#14065=CARTESIAN_POINT ( 'NONE',  ( -7.500000000000000000, -3.988190556646204588, -0.8526458641284329065 ) ) ;
#14073=CARTESIAN_POINT ( 'NONE',  ( 7.908217798048221781, 3.084840533507044125, -7.795645399445156443 ) ) ;
#14099=CARTESIAN_POINT ( 'NONE',  ( 1.211595439868046853, -7.960739084487661543, -0.4504974108212073114 ) ) ;
#14101=ORIENTED_EDGE ( 'NONE', *, *, #22136, .T. ) ;
#14110=CONICAL_SURFACE ( 'NONE', #17533, 7.500000000000001776, 0.8594454914424796144 ) ;
#14143=AXIS2_PLACEMENT_3D ( 'NONE', #7123, #12850, #5316 ) ;
#14157=CIRCLE ( 'NONE', #6413, 5.000000000000001776 ) ;
#14167=CARTESIAN_POINT ( 'NONE',  ( 3.295171437449806451, 7.213553046161976567, -7.590212325761626744 ) ) ;
#14182=EDGE_CURVE ( 'NONE', #16635, #19884, #22061, .T. ) ;
#14211=CARTESIAN_POINT ( 'NONE',  ( -1.994931997373328159E-14, -8.660254037844390851, -1.000000000000000888 ) ) ;
#14219=AXIS2_PLACEMENT_3D ( 'NONE', #7762, #13117, #9818 ) ;
#14232=DIRECTION ( 'NONE',  ( 1.000000000000000000, 0.000000000000000000, -0.000000000000000000 ) ) ;
#14233=VERTEX_POINT ( 'NONE', #2611 ) ;
#14245=CARTESIAN_POINT ( 'NONE',  ( 6.293430271071537518, -5.026740376715104652, -0.4524126574264552558 ) ) ;
#14251=EDGE_LOOP ( 'NONE', ( #1388, #1369, #3216, #23629, #20861, #4756, #23589 ) ) ;
#14271=EDGE_LOOP ( 'NONE', ( #6227, #10075, #4357, #7995 ) ) ;
#14284=FACE_OUTER_BOUND ( 'NONE', #6972, .T. ) ;
#14288=VECTOR ( 'NONE', #100, 1000.000000000000000 ) ;
#14291=EDGE_LOOP ( 'NONE', ( #9073, #12936, #17189, #14570 ) ) ;
#14324=ORIENTED_EDGE ( 'NONE', *, *, #20932, .T. ) ;
#14344=CARTESIAN_POINT ( 'NONE',  ( -7.500000000000000888, 2.886751345948126435, -7.198902722707427593 ) ) ;
#14352=EDGE_CURVE ( 'NONE', #19450, #1864, #15018, .T. ) ;
#14374=VERTEX_POINT ( 'NONE', #8300 ) ;
#14389=VERTEX_POINT ( 'NONE', #6360 ) ;
#14415=ORIENTED_EDGE ( 'NONE', *, *, #3626, .T. ) ;
#14451=DIRECTION ( 'NONE',  ( 0.8660254037844381525, -0.5000000000000007772, 0.000000000000000000 ) ) ;
#14485=CARTESIAN_POINT ( 'NONE',  ( 2.452879891156805492, 7.244083172395185954, -0.1007566405101774504 ) ) ;
#14498=DIRECTION ( 'NONE',  ( -0.000000000000000000, -0.000000000000000000, 1.000000000000000000 ) ) ;
#14529=ORIENTED_EDGE ( 'NONE', *, *, #12630, .T. ) ;
#14537=EDGE_CURVE ( 'NONE', #16635, #9210, #3580, .T. ) ;
#14547=ORIENTED_EDGE ( 'NONE', *, *, #21980, .T. ) ;
#14548=CONICAL_SURFACE ( 'NONE', #4105, 7.500000000000001776, 0.8594454914424796144 ) ;
#14555=SURFACE_STYLE_FILL_AREA ( #8999 ) ;
#14559=( BOUNDED_SURFACE ( )  B_SPLINE_SURFACE ( 3, 2, ( 
 ( #14051, #8712, #21381 ),
 ( #4840, #3013, #10425 ),
 ( #17775, #1220, #8592 ),
 ( #18002, #23306, #14167 ),
 ( #21636, #1449, #16427 ),
 ( #5443, #12729, #19923 ),
 ( #23780, #14623, #9423 ),
 ( #13082, #3372, #20048 ) ),
 .UNSPECIFIED., .F., .F., .F. ) 
 B_SPLINE_SURFACE_WITH_KNOTS ( ( 4, 2, 2, 4 ),
 ( 3, 3 ),
 ( 0.03861844051980969222, 0.04325213341840641185, 0.04556897986770477166, 0.04788582631700313147 ),
 ( 0.000000000000000000, 1.000000000000000000 ),
 .UNSPECIFIED. ) 
 GEOMETRIC_REPRESENTATION_ITEM ( )  RATIONAL_B_SPLINE_SURFACE ( (
 ( 1.000000000000000000, 0.8047781759831921233, 1.000000000000000000),
 ( 1.000000000000000000, 0.8123762462806503049, 1.000000000000000000),
 ( 1.000000000000000000, 0.8190659850614813164, 1.000000000000000000),
 ( 1.000000000000000000, 0.8191937571014595854, 1.000000000000000000),
 ( 1.000000000000000000, 0.8176092952779865364, 1.000000000000000000),
 ( 1.000000000000000000, 0.8122962088597069918, 1.000000000000000000),
 ( 1.000000000000000000, 0.8086311330827506971, 1.000000000000000000),
 ( 1.000000000000000000, 0.8047712282214323221, 1.000000000000000000) ) ) 
 REPRESENTATION_ITEM ( '' )  SURFACE ( )  );
#14570=ORIENTED_EDGE ( 'NONE', *, *, #1150, .F. ) ;
#14578=CARTESIAN_POINT ( 'NONE',  ( -2.352990130084580066E-16, 8.660254037844390851, -10.00000000000000000 ) ) ;
#14589=CARTESIAN_POINT ( 'NONE',  ( 6.486836893983020325, -4.915077010914103539, -7.231838333420563814 ) ) ;
#14594=ORIENTED_EDGE ( 'NONE', *, *, #18012, .F. ) ;
#14596=CARTESIAN_POINT ( 'NONE',  ( -2.352990130084580066E-16, 8.660254037844390851, -7.422398894150034288 ) ) ;
#14602=CARTESIAN_POINT ( 'NONE',  ( 7.922281120364393914, 4.573931137438269623, -8.047472243342930653 ) ) ;
#14617=AXIS2_PLACEMENT_3D ( 'NONE', #9234, #5595, #3419 ) ;
#14623=CARTESIAN_POINT ( 'NONE',  ( 0.3875187462248268488, 8.436519985393664101, -7.781689322726965230 ) ) ;
#14658=VECTOR ( 'NONE', #2705, 1000.000000000000000 ) ;
#14722=B_SPLINE_CURVE_WITH_KNOTS ( 'NONE', 3,
 ( #6198, #11668, #18511, #162, #13483, #18973, #2439, #9829, #18857 ),
 .UNSPECIFIED., .F., .F.,
 ( 4, 2, 1, 2, 4 ),
 ( 0.000000000000000000, 0.002165063509461097498, 0.004330127018922194995, 0.006495190528383292493, 0.008660254037844389990 ),
 .UNSPECIFIED. ) ;
#14741=ORIENTED_EDGE ( 'NONE', *, *, #1235, .T. ) ;
#14764=DIRECTION ( 'NONE',  ( -0.000000000000000000, -0.000000000000000000, 1.000000000000000000 ) ) ;
#14799=CARTESIAN_POINT ( 'NONE',  ( -7.500000000000000000, -2.886751345948133984, -7.198902722707428481 ) ) ;
#14806=CARTESIAN_POINT ( 'NONE',  ( 7.499999999999999112, 1.854554393013827296, -0.1880126015361732184 ) ) ;
#14820=CARTESIAN_POINT ( 'NONE',  ( -5.047120108843199837, 5.746297884371392328, -0.1007566405101777279 ) ) ;
#14828=ORIENTED_EDGE ( 'NONE', *, *, #8114, .F. ) ;
#14850=CARTESIAN_POINT ( 'NONE',  ( 7.907996613752301229, 3.055722423191984838, -7.792112796859423263 ) ) ;
#14866=ORIENTED_EDGE ( 'NONE', *, *, #15166, .F. ) ;
#14871=CARTESIAN_POINT ( 'NONE',  ( 0.000000000000000000, 0.000000000000000000, -8.499999999999998224 ) ) ;
#14882=DIRECTION ( 'NONE',  ( 1.000000000000000000, 0.000000000000000000, 0.000000000000000000 ) ) ;
#14914=DIRECTION ( 'NONE',  ( 0.000000000000000000, 0.000000000000000000, 1.000000000000000000 ) ) ;
#15011=EDGE_LOOP ( 'NONE', ( #9266, #10827, #13347 ) ) ;
#15018=CIRCLE ( 'NONE', #18477, 5.000000000000000888 ) ;
#15030=CIRCLE ( 'NONE', #22325, 7.500000000000001776 ) ;
#15040=CIRCLE ( 'NONE', #6544, 10.39117206796836079 ) ;
#15073=CARTESIAN_POINT ( 'NONE',  ( -7.499999999999650058, -0.7583608255766450812, -7.446489218764574147 ) ) ;
#15075=PRODUCT_DEFINITION_FORMATION_WITH_SPECIFIED_SOURCE ( 'ANY', '', #6496, .NOT_KNOWN. ) ;
#15099=FACE_OUTER_BOUND ( 'NONE', #15011, .T. ) ;
#15146=ADVANCED_FACE ( 'NONE', ( #13995 ), #21320, .T. ) ;
#15166=EDGE_CURVE ( 'NONE', #2346, #16143, #19403, .T. ) ;
#15186=CARTESIAN_POINT ( 'NONE',  ( -7.499999999999999112, -4.652405105468739421, -7.929127756970856034 ) ) ;
#15203=EDGE_CURVE ( 'NONE', #16635, #23462, #5308, .T. ) ;
#15212=CARTESIAN_POINT ( 'NONE',  ( -7.298354728638373423, 4.926141412641537265, -7.913704048100170141 ) ) ;
#15238=CARTESIAN_POINT ( 'NONE',  ( 10.39117206796836079, 1.272551561242683567E-15, -8.499999999999998224 ) ) ;
#15387=DIRECTION ( 'NONE',  ( -0.9396926207859143121, 0.000000000000000000, -0.3420201433256525592 ) ) ;
#15421=CARTESIAN_POINT ( 'NONE',  ( 5.040301471719072168, 5.750234626350511746, -0.09933465333851003443 ) ) ;
#15483=EDGE_LOOP ( 'NONE', ( #16856, #465, #17390 ) ) ;
#15501=CARTESIAN_POINT ( 'NONE',  ( 7.500000000000000000, -3.608439182435168036, -7.298562697733107285 ) ) ;
#15512=CARTESIAN_POINT ( 'NONE',  ( -5.276765049035075705, 6.073111908730296271, -7.634085501268424778 ) ) ;
#15521=CARTESIAN_POINT ( 'NONE',  ( 7.500000000000000000, 4.732328341851997244, -7.493855119309152713 ) ) ;
#15538=ORIENTED_EDGE ( 'NONE', *, *, #10905, .F. ) ;
#15600=CIRCLE ( 'NONE', #19420, 10.12668159690567649 ) ;
#15609=STYLED_ITEM('',(#23927),#12097);
#15621=CARTESIAN_POINT ( 'NONE',  ( -2.623433461001184686, 7.604994000793856124, -7.633824513837113912 ) ) ;
#15631=CARTESIAN_POINT ( 'NONE',  ( -2.352990130084580066E-16, 8.660254037844390851, -7.422398894150034288 ) ) ;
#15644=EDGE_LOOP ( 'NONE', ( #21797, #13955, #21908, #17181 ) ) ;
#15711=DIRECTION ( 'NONE',  ( -1.000000000000000000, 0.000000000000000000, 0.000000000000000000 ) ) ;
#15721=ORIENTED_EDGE ( 'NONE', *, *, #19798, .T. ) ;
#15743=CARTESIAN_POINT ( 'NONE',  ( 7.500000000000000000, -1.645076096015019695, -7.030022527230891605 ) ) ;
#15750=EDGE_LOOP ( 'NONE', ( #4579, #16693, #13530, #15721, #17036 ) ) ;
#15757=EDGE_LOOP ( 'NONE', ( #14547, #20908, #14741, #5545 ) ) ;
#15785=B_SPLINE_CURVE_WITH_KNOTS ( 'NONE', 3,
 ( #10700, #246, #9431, #11147, #7602, #13087, #22335, #22084, #19723, #11273 ),
 .UNSPECIFIED., .F., .F.,
 ( 4, 2, 2, 2, 4 ),
 ( 0.000000000000000000, 0.002305503304226489900, 0.004611006608452982401, 0.006916509912679474036, 0.009222013216905966537 ),
 .UNSPECIFIED. ) ;
#15803=CARTESIAN_POINT ( 'NONE',  ( -6.250000000000000000, -5.051814855409233473, -7.198902722707430257 ) ) ;
#15858=ADVANCED_FACE ( 'NONE', ( #2004 ), #10698, .F. ) ;
#15879=B_SPLINE_CURVE_WITH_KNOTS ( 'NONE', 3,
 ( #19879, #20337, #5505, #3800, #16631, #18540 ),
 .UNSPECIFIED., .F., .F.,
 ( 4, 2, 4 ),
 ( -5.145455527297706927E-06, 0.0004153350442917282917, 0.0008358155441107560776 ),
 .UNSPECIFIED. ) ;
#15897=CARTESIAN_POINT ( 'NONE',  ( 3.750000000000004441, -6.495190528383289141, 0.000000000000000000 ) ) ;
#15944=CARTESIAN_POINT ( 'NONE',  ( -7.914973979435149687, -3.817460047930451239, -7.907502498112421563 ) ) ;
#15963=AXIS2_PLACEMENT_3D ( 'NONE', #14871, #22205, #13579 ) ;
#16013=( LENGTH_UNIT ( ) NAMED_UNIT ( * ) SI_UNIT ( .MILLI., .METRE. ) );
#16015=DIRECTION ( 'NONE',  ( -0.8660254037844382635, 0.5000000000000005551, 0.000000000000000000 ) ) ;
#16044=ORIENTED_EDGE ( 'NONE', *, *, #12991, .T. ) ;
#16087=CARTESIAN_POINT ( 'NONE',  ( 7.549006887134069643, -4.358421158401204032, -7.700127545397312367 ) ) ;
#16109=PRODUCT_DEFINITION ( 'UNKNOWN', '', #15075, #3716 ) ;
#16143=VERTEX_POINT ( 'NONE', #17695 ) ;
#16218=EDGE_CURVE ( 'NONE', #8135, #5418, #23367, .T. ) ;
#16225=CARTESIAN_POINT ( 'NONE',  ( -7.500000000000001776, 0.000000000000000000, 0.000000000000000000 ) ) ;
#16287=EDGE_LOOP ( 'NONE', ( #17430, #7332, #13233, #4810, #7108 ) ) ;
#16318=DIRECTION ( 'NONE',  ( 0.000000000000000000, 0.000000000000000000, -1.000000000000000000 ) ) ;
#16330=CARTESIAN_POINT ( 'NONE',  ( -7.499999999999999112, -2.930060224340425901, -0.4701183149080249146 ) ) ;
#16331=ORIENTED_EDGE ( 'NONE', *, *, #10710, .T. ) ;
#16374=ORIENTED_EDGE ( 'NONE', *, *, #16218, .T. ) ;
#16376=ORIENTED_EDGE ( 'NONE', *, *, #23770, .T. ) ;
#16389=CARTESIAN_POINT ( 'NONE',  ( -7.500000000000000000, -4.330127018922198090, -10.00000000000000000 ) ) ;
#16392=ADVANCED_FACE ( 'NONE', ( #3312 ), #1508, .T. ) ;
#16395=CARTESIAN_POINT ( 'NONE',  ( 4.599534470797546959, -6.460478697736932396, -7.590212325761396706 ) ) ;
#16408=CARTESIAN_POINT ( 'NONE',  ( 7.703928834700305650, 4.447865386531936416, -7.917997657324733929 ) ) ;
#16411=EDGE_CURVE ( 'NONE', #4336, #5418, #14157, .T. ) ;
#16422=AXIS2_PLACEMENT_3D ( 'NONE', #2785, #19807, #3257 ) ;
#16427=CARTESIAN_POINT ( 'NONE',  ( 2.621328321948289020, 7.606199919103058704, -7.633618187056857352 ) ) ;
#16444=EDGE_LOOP ( 'NONE', ( #3981, #10206, #6651, #5612 ) ) ;
#16449=B_SPLINE_CURVE_WITH_KNOTS ( 'NONE', 3,
 ( #17591, #1041, #15803, #17956, #5271, #6975, #18408, #11087, #7320 ),
 .UNSPECIFIED., .F., .F.,
 ( 4, 2, 1, 2, 4 ),
 ( 0.000000000000000000, 0.002165063509461097064, 0.004330127018922194128, 0.006495190528383290758, 0.008660254037844389990 ),
 .UNSPECIFIED. ) ;
#16498=VECTOR ( 'NONE', #7674, 1000.000000000000000 ) ;
#16508=CARTESIAN_POINT ( 'NONE',  ( 7.169303301815196150, -4.521054846639319003, -7.349897473155491134 ) ) ;
#16512=DIRECTION ( 'NONE',  ( 0.5000000000000005551, -0.8660254037844383745, 0.000000000000000000 ) ) ;
#16609=CARTESIAN_POINT ( 'NONE',  ( -7.500000000000001776, 2.932633423934442263, -0.4709827563909292358 ) ) ;
#16611=ADVANCED_FACE ( 'NONE', ( #21404 ), #771, .F. ) ;
#16631=CARTESIAN_POINT ( 'NONE',  ( -7.500000000000005329, 4.330127018922187432, -7.564335161054492218 ) ) ;
#16635=VERTEX_POINT ( 'NONE', #17437 ) ;
#16693=ORIENTED_EDGE ( 'NONE', *, *, #9571, .T. ) ;
#16720=CIRCLE ( 'NONE', #6302, 10.12668159690567649 ) ;
#16742=CARTESIAN_POINT ( 'NONE',  ( -7.500000000000698996, 1.613867362005801054, -7.450195926347907616 ) ) ;
#16748=CARTESIAN_POINT ( 'NONE',  ( 5.088535779737119569, -5.722386535631984295, -7.491772860715834703 ) ) ;
#16755=CARTESIAN_POINT ( 'NONE',  ( -5.007715329123872641E-16, -8.660254037844399733, -10.00000000000000000 ) ) ;
#16807=VERTEX_POINT ( 'NONE', #2058 ) ;
#16813=CARTESIAN_POINT ( 'NONE',  ( -7.922281120364393914, -4.573931137438277617, -8.047472243342932430 ) ) ;
#16856=ORIENTED_EDGE ( 'NONE', *, *, #1199, .F. ) ;
#16928=ORIENTED_EDGE ( 'NONE', *, *, #12294, .T. ) ;
#17029=CARTESIAN_POINT ( 'NONE',  ( -6.288404560131954923, -5.029641972278938944, -0.4504974108212008721 ) ) ;
#17036=ORIENTED_EDGE ( 'NONE', *, *, #6674, .T. ) ;
#17040=ADVANCED_FACE ( 'NONE', ( #1447 ), #14548, .T. ) ;
#17049=CARTESIAN_POINT ( 'NONE',  ( -7.777900015783941967, -4.169681370001537601, -7.928862157988302073 ) ) ;
#17090=ORIENTED_EDGE ( 'NONE', *, *, #999, .F. ) ;
#17155=B_SPLINE_CURVE_WITH_KNOTS ( 'NONE', 3,
 ( #23384, #6843, #14245, #21585, #3205, #18406 ),
 .UNSPECIFIED., .F., .F.,
 ( 4, 2, 4 ),
 ( 2.475503369227215526E-07, 0.002222330217055624568, 0.004444412883774326306 ),
 .UNSPECIFIED. ) ;
#17160=ORIENTED_EDGE ( 'NONE', *, *, #13801, .T. ) ;
#17161=CARTESIAN_POINT ( 'NONE',  ( 0.2791032213812723040, -8.821394357840571132, -7.929128246061910801 ) ) ;
#17175=DIRECTION ( 'NONE',  ( -0.000000000000000000, -0.000000000000000000, 1.000000000000000000 ) ) ;
#17181=ORIENTED_EDGE ( 'NONE', *, *, #6246, .F. ) ;
#17189=ORIENTED_EDGE ( 'NONE', *, *, #14352, .T. ) ;
#17211=DIRECTION ( 'NONE',  ( 0.000000000000000000, 0.000000000000000000, -1.000000000000000000 ) ) ;
#17223=CARTESIAN_POINT ( 'NONE',  ( -7.500000000000000000, -0.7729939684941458111, -7.026407045654831762 ) ) ;
#17270=EDGE_LOOP ( 'NONE', ( #23056, #14008, #1985, #2857, #6883, #9065, #2572 ) ) ;
#17299=AXIS2_PLACEMENT_3D ( 'NONE', #4093, #11506, #23388 ) ;
#17319=CARTESIAN_POINT ( 'NONE',  ( 7.499999999997997158, -3.157198044624895061, -7.642795354507847527 ) ) ;
#17328=PLANE ( 'NONE',  #20320 ) ;
#17382=CARTESIAN_POINT ( 'NONE',  ( -0.5984201754795734907, -8.314755988442763979, -0.7022220667781372549 ) ) ;
#17383=AXIS2_PLACEMENT_3D ( 'NONE', #10160, #2997, #17867 ) ;
#17390=ORIENTED_EDGE ( 'NONE', *, *, #219, .F. ) ;
#17405=CARTESIAN_POINT ( 'NONE',  ( 4.613983237546155358, -6.452243898629820507, -7.591546097228409451 ) ) ;
#17430=ORIENTED_EDGE ( 'NONE', *, *, #9440, .T. ) ;
#17432=CARTESIAN_POINT ( 'NONE',  ( 7.894705354777835637, 0.7527931906242791849, -7.590204373988219011 ) ) ;
#17434=EDGE_CURVE ( 'NONE', #19296, #17922, #5621, .T. ) ;
#17437=CARTESIAN_POINT ( 'NONE',  ( -5.007715329123872641E-16, -8.660254037844399733, -7.422398894150038728 ) ) ;
#17483=DIRECTION ( 'NONE',  ( 1.224646799147353207E-16, 1.000000000000000000, 0.000000000000000000 ) ) ;
#17496=EDGE_LOOP ( 'NONE', ( #19653, #13997, #18902 ) ) ;
#17503=DIRECTION ( 'NONE',  ( 0.000000000000000000, 0.000000000000000000, -1.000000000000000000 ) ) ;
#17533=AXIS2_PLACEMENT_3D ( 'NONE', #8351, #19692, #8717 ) ;
#17538=CARTESIAN_POINT ( 'NONE',  ( -3.750000000000001776, 6.495190528383289141, -6.991905250253753756 ) ) ;
#17569=CARTESIAN_POINT ( 'NONE',  ( -7.640563834021360018E-16, -9.147862274876560562, -8.047472243342937759 ) ) ;
#17591=CARTESIAN_POINT ( 'NONE',  ( -7.500000000000000000, -4.330127018922198090, -7.422398894150034288 ) ) ;
#17623=ADVANCED_FACE ( 'NONE', ( #11799 ), #17328, .T. ) ;
#17647=ADVANCED_BREP_SHAPE_REPRESENTATION ( '', ( #12097, #11210 ), #370 ) ;
#17664=AXIS2_PLACEMENT_3D ( 'NONE', #20032, #23415, #5081 ) ;
#17676=CARTESIAN_POINT ( 'NONE',  ( -7.894787914004607998, -1.230850257101226302E-13, -7.591390474663425536 ) ) ;
#17681=DIRECTION ( 'NONE',  ( -1.000000000000000000, 0.000000000000000000, 0.000000000000000000 ) ) ;
#17687=( NAMED_UNIT ( * ) SI_UNIT ( $, .STERADIAN. ) SOLID_ANGLE_UNIT ( ) );
#17691=CONICAL_SURFACE ( 'NONE', #12014, 7.500000000000001776, 0.8594454914424796144 ) ;
#17695=CARTESIAN_POINT ( 'NONE',  ( 7.922281120364393914, -4.573931137438282057, -8.047472243342932430 ) ) ;
#17713=EDGE_CURVE ( 'NONE', #7849, #6769, #19442, .T. ) ;
#17722=CARTESIAN_POINT ( 'NONE',  ( -1.206569728928481577, -7.963640680051488729, -0.4524126574264552558 ) ) ;
#17733=CIRCLE ( 'NONE', #5387, 7.500000000000001776 ) ;
#17764=CARTESIAN_POINT ( 'NONE',  ( -2.352174619740013739, 7.302225387956623237, -7.450218641348505422 ) ) ;
#17765=CARTESIAN_POINT ( 'NONE',  ( 5.000000000000000888, 0.000000000000000000, -25.03750572909317285 ) ) ;
#17770=CIRCLE ( 'NONE', #781, 7.500000000000001776 ) ;
#17775=CARTESIAN_POINT ( 'NONE',  ( 5.174575781541291164, 5.672711317429402378, -7.030005583190089169 ) ) ;
#17794=CARTESIAN_POINT ( 'NONE',  ( 7.500000000000000000, 1.545478204151513157, -7.491761935628701075 ) ) ;
#17800=CARTESIAN_POINT ( 'NONE',  ( 7.499999999999999112, -4.330127018922205195, -1.000000000000000888 ) ) ;
#17861=LINE ( 'NONE', #21724, #17883 ) ;
#17867=DIRECTION ( 'NONE',  ( 1.000000000000000000, 0.000000000000000000, 0.000000000000000000 ) ) ;
#17883=VECTOR ( 'NONE', #20022, 1000.000000000000114 ) ;
#17905=ADVANCED_FACE ( 'NONE', ( #5231 ), #9094, .F. ) ;
#17910=CARTESIAN_POINT ( 'NONE',  ( 7.500000000000000888, -0.7512838658081439913, 1.423015351387224570E-15 ) ) ;
#17922=VERTEX_POINT ( 'NONE', #3285 ) ;
#17923=DIRECTION ( 'NONE',  ( 0.000000000000000000, 0.000000000000000000, 1.000000000000000000 ) ) ;
#17935=CARTESIAN_POINT ( 'NONE',  ( 2.499999999999999112, -7.216878364870334295, -7.063244554130005959 ) ) ;
#17956=CARTESIAN_POINT ( 'NONE',  ( -5.000000000000000000, -5.773502691896264416, -7.063244554130003294 ) ) ;
#17998=DIRECTION ( 'NONE',  ( 1.000000000000000000, 0.000000000000000000, 0.000000000000000000 ) ) ;
#18002=CARTESIAN_POINT ( 'NONE',  ( 3.080866544135574259, 6.881514909250401324, -7.026396753507782478 ) ) ;
#18005=EDGE_CURVE ( 'NONE', #2744, #23060, #690, .T. ) ;
#18012=EDGE_CURVE ( 'NONE', #8135, #11056, #8022, .T. ) ;
#18054=CARTESIAN_POINT ( 'NONE',  ( -7.499999999999999112, 1.443375672974061219, -7.063244554130000630 ) ) ;
#18073=CARTESIAN_POINT ( 'NONE',  ( -6.901579824520442941, 4.675625068323816080, -0.7022220667781327030 ) ) ;
#18077=CARTESIAN_POINT ( 'NONE',  ( -7.500000000000000000, 4.330127018922191873, -0.9999999999999970024 ) ) ;
#18103=ORIENTED_EDGE ( 'NONE', *, *, #22133, .F. ) ;
#18130=ORIENTED_EDGE ( 'NONE', *, *, #14537, .T. ) ;
#18137=EDGE_CURVE ( 'NONE', #14233, #13071, #23709, .T. ) ;
#18158=DIRECTION ( 'NONE',  ( 0.000000000000000000, 0.000000000000000000, 1.000000000000000000 ) ) ;
#18168=FACE_OUTER_BOUND ( 'NONE', #14291, .T. ) ;
#18172=ORIENTED_EDGE ( 'NONE', *, *, #11700, .F. ) ;
#18173=CARTESIAN_POINT ( 'NONE',  ( -7.500000000000000000, -4.330127018922199866, -1.000000000000000888 ) ) ;
#18193=CARTESIAN_POINT ( 'NONE',  ( -3.750000000000004885, 6.495190528383289141, 0.000000000000000000 ) ) ;
#18195=DIRECTION ( 'NONE',  ( 1.000000000000000000, 0.000000000000000000, 0.000000000000000000 ) ) ;
#18203=CARTESIAN_POINT ( 'NONE',  ( -0.3470952277635217520, -8.860649561028104415, -7.493596212620245112 ) ) ;
#18209=CARTESIAN_POINT ( 'NONE',  ( 3.093157300003884558, 6.874418838041288282, 2.127746763502802452E-15 ) ) ;
#18291=ORIENTED_EDGE ( 'NONE', *, *, #17434, .F. ) ;
#18327=CARTESIAN_POINT ( 'NONE',  ( 7.894787914004607998, 1.243647571710251278E-13, -7.591390474663425536 ) ) ;
#18388=CARTESIAN_POINT ( 'NONE',  ( 7.897850199329715437, -1.533397866934079312, -7.634054012537967893 ) ) ;
#18402=CARTESIAN_POINT ( 'NONE',  ( 0.000000000000000000, 0.000000000000000000, -0.5251556536572846712 ) ) ;
#18406=CARTESIAN_POINT ( 'NONE',  ( 3.750000000000004441, -6.495190528383289141, 0.000000000000000000 ) ) ;
#18408=CARTESIAN_POINT ( 'NONE',  ( -1.250000000000000444, -7.938566201357367902, -7.198902722707430257 ) ) ;
#18422=CARTESIAN_POINT ( 'NONE',  ( 1.015826369459276846, -8.073766409988136772, -7.642786413614194529 ) ) ;
#18428=VECTOR ( 'NONE', #9434, 1000.000000000000000 ) ;
#18441=CARTESIAN_POINT ( 'NONE',  ( 7.897836333153806621, 1.530409084195003988, -7.633857274177628049 ) ) ;
#18474=ORIENTED_EDGE ( 'NONE', *, *, #20932, .F. ) ;
#18477=AXIS2_PLACEMENT_3D ( 'NONE', #22655, #13549, #1029 ) ;
#18511=CARTESIAN_POINT ( 'NONE',  ( 6.250000000000000888, 5.051814855409225480, -7.198902722707425816 ) ) ;
#18535=ORIENTED_EDGE ( 'NONE', *, *, #925, .T. ) ;
#18540=CARTESIAN_POINT ( 'NONE',  ( -7.500000000000000000, 4.330127018922191873, -7.422398894150032511 ) ) ;
#18546=VERTEX_POINT ( 'NONE', #5045 ) ;
#18593=CARTESIAN_POINT ( 'NONE',  ( -4.250000000000000000, 5.204748896376250699E-16, -9.449444346342714240 ) ) ;
#18648=DIRECTION ( 'NONE',  ( -0.000000000000000000, -0.000000000000000000, -1.000000000000000000 ) ) ;
#18651=ORIENTED_EDGE ( 'NONE', *, *, #15203, .T. ) ;
#18759=CARTESIAN_POINT ( 'NONE',  ( -1.994931997373328159E-14, -8.660254037844390851, -1.000000000000000888 ) ) ;
#18846=ADVANCED_FACE ( 'NONE', ( #18887 ), #6777, .T. ) ;
#18857=CARTESIAN_POINT ( 'NONE',  ( -2.352990130084580066E-16, 8.660254037844390851, -7.422398894150034288 ) ) ;
#18887=FACE_OUTER_BOUND ( 'NONE', #14251, .T. ) ;
#18900=CARTESIAN_POINT ( 'NONE',  ( 7.499999999999999112, -4.330127018922205195, -1.000000000000000888 ) ) ;
#18902=ORIENTED_EDGE ( 'NONE', *, *, #19798, .F. ) ;
#18945=ORIENTED_EDGE ( 'NONE', *, *, #23770, .F. ) ;
#18951=FACE_OUTER_BOUND ( 'NONE', #20940, .T. ) ;
#18955=CARTESIAN_POINT ( 'NONE',  ( -3.093533885184598375, -6.874201416485457017, -7.446478553994068328 ) ) ;
#18973=CARTESIAN_POINT ( 'NONE',  ( 2.500000000000000444, 7.216878364870322748, -7.063244554130000630 ) ) ;
#19048=EDGE_CURVE ( 'NONE', #18546, #6258, #10469, .T. ) ;
#19099=B_SPLINE_CURVE_WITH_KNOTS ( 'NONE', 3,
 ( #6947, #1012, #7053, #14099, #10340, #14211 ),
 .UNSPECIFIED., .F., .F.,
 ( 4, 2, 4 ),
 ( 0.004444412883774326306, 0.006655097293744431999, 0.008865781703714537693 ),
 .UNSPECIFIED. ) ;
#19153=EDGE_CURVE ( 'NONE', #9210, #4056, #15785, .T. ) ;
#19182=DIRECTION ( 'NONE',  ( 1.000000000000000000, 0.000000000000000000, -0.000000000000000000 ) ) ;
#19187=CARTESIAN_POINT ( 'NONE',  ( -7.640563834021360018E-16, -9.147862274876560562, -8.047472243342937759 ) ) ;
#19199=ORIENTED_EDGE ( 'NONE', *, *, #20180, .F. ) ;
#19202=CARTESIAN_POINT ( 'NONE',  ( 7.500000000000000000, 4.330127018922190096, -7.422398894150032511 ) ) ;
#19225=CARTESIAN_POINT ( 'NONE',  ( -5.000000000000000888, 5.773502691896258199, -7.063244554130002406 ) ) ;
#19231=DIRECTION ( 'NONE',  ( 1.000000000000000000, 0.000000000000000000, 0.000000000000000000 ) ) ;
#19295=CARTESIAN_POINT ( 'NONE',  ( -5.007715329123872641E-16, -8.660254037844399733, -7.422398894150038728 ) ) ;
#19296=VERTEX_POINT ( 'NONE', #10159 ) ;
#19343=CARTESIAN_POINT ( 'NONE',  ( 7.922798488042200660, -4.627419312545550056, -8.057411459260041653 ) ) ;
#19346=CARTESIAN_POINT ( 'NONE',  ( 7.500000000000000000, 4.330127018922190096, -10.00000000000000000 ) ) ;
#19359=DIRECTION ( 'NONE',  ( 0.000000000000000000, 0.000000000000000000, 1.000000000000000000 ) ) ;
#19395=CARTESIAN_POINT ( 'NONE',  ( -3.093157300003891663, -6.874418838041293611, -6.051203375184721622E-15 ) ) ;
#19403=B_SPLINE_CURVE_WITH_KNOTS ( 'NONE', 3,
 ( #11068, #6953, #18388, #1727, #9001, #23486 ),
 .UNSPECIFIED., .F., .F.,
 ( 4, 2, 4 ),
 ( 0.004615310220740742597, 0.006918661718823353700, 0.009222013216905964803 ),
 .UNSPECIFIED. ) ;
#19405=DIRECTION ( 'NONE',  ( 0.000000000000000000, 0.000000000000000000, -1.000000000000000000 ) ) ;
#19420=AXIS2_PLACEMENT_3D ( 'NONE', #9624, #13165, #12915 ) ;
#19432=LINE ( 'NONE', #12499, #3304 ) ;
#19442=B_SPLINE_CURVE_WITH_KNOTS ( 'NONE', 3,
 ( #17800, #1361, #8261, #23217, #10572, #6802, #17910, #21526 ),
 .UNSPECIFIED., .F., .F.,
 ( 4, 2, 2, 4 ),
 ( 0.006061689441712453386, 0.007174127271521678166, 0.008286565101330902947, 0.01051144076094935251 ),
 .UNSPECIFIED. ) ;
#19445=ORIENTED_EDGE ( 'NONE', *, *, #19048, .F. ) ;
#19450=VERTEX_POINT ( 'NONE', #20141 ) ;
#19479=EDGE_CURVE ( 'NONE', #5970, #2346, #7821, .T. ) ;
#19500=B_SPLINE_CURVE_WITH_KNOTS ( 'NONE', 3,
 ( #15631, #2703, #1237, #6315, #17538, #19225, #6794, #23329, #19573 ),
 .UNSPECIFIED., .F., .F.,
 ( 4, 2, 1, 2, 4 ),
 ( 0.000000000000000000, 0.002165063509461098365, 0.004330127018922195863, 0.006495190528383293360, 0.008660254037844389990 ),
 .UNSPECIFIED. ) ;
#19529=CARTESIAN_POINT ( 'NONE',  ( 4.336808689942017736E-16, 8.660254037844390851, -1.000000000000000888 ) ) ;
#19541=FACE_OUTER_BOUND ( 'NONE', #7616, .T. ) ;
#19555=CARTESIAN_POINT ( 'NONE',  ( 0.000000000000000000, 0.000000000000000000, 0.000000000000000000 ) ) ;
#19562=AXIS2_PLACEMENT_3D ( 'NONE', #3990, #17175, #7994 ) ;
#19573=CARTESIAN_POINT ( 'NONE',  ( -7.500000000000000000, 4.330127018922191873, -7.422398894150032511 ) ) ;
#19589=CARTESIAN_POINT ( 'NONE',  ( 7.894787914004607998, 1.243647571710251278E-13, -7.591390474663425536 ) ) ;
#19591=ADVANCED_FACE ( 'NONE', ( #15099 ), #1858, .T. ) ;
#19601=CARTESIAN_POINT ( 'NONE',  ( -7.914984360234579519, 3.818534719232089980, -7.907701344400639876 ) ) ;
#19621=CONICAL_SURFACE ( 'NONE', #6517, 4.174999999999999822, 0.9599310885968795892 ) ;
#19636=ORIENTED_EDGE ( 'NONE', *, *, #8151, .F. ) ;
#19653=ORIENTED_EDGE ( 'NONE', *, *, #9381, .F. ) ;
#19680=CARTESIAN_POINT ( 'NONE',  ( -5.112021521198522933, 5.708827036477257977, -7.069802615102034338 ) ) ;
#19692=DIRECTION ( 'NONE',  ( 0.000000000000000000, 0.000000000000000000, -1.000000000000000000 ) ) ;
#19723=CARTESIAN_POINT ( 'NONE',  ( -7.263825692932299738, -4.945657111639584436, -7.907570769506049757 ) ) ;
#19726=CARTESIAN_POINT ( 'NONE',  ( -7.500000000000000000, 4.330127018922191873, -10.00000000000000000 ) ) ;
#19737=CARTESIAN_POINT ( 'NONE',  ( 4.999999999999999112, -5.773502691896267081, -7.063244554130005071 ) ) ;
#19764=ORIENTED_EDGE ( 'NONE', *, *, #20135, .F. ) ;
#19785=VERTEX_POINT ( 'NONE', #10732 ) ;
#19798=EDGE_CURVE ( 'NONE', #6258, #6350, #8136, .T. ) ;
#19802=FACE_OUTER_BOUND ( 'NONE', #5149, .T. ) ;
#19807=DIRECTION ( 'NONE',  ( 0.000000000000000000, 0.000000000000000000, -1.000000000000000000 ) ) ;
#19812=CARTESIAN_POINT ( 'NONE',  ( 5.000000000000001776, 6.123233995736768255E-16, -9.974600000000000577 ) ) ;
#19813=ORIENTED_EDGE ( 'NONE', *, *, #21980, .F. ) ;
#19868=FACE_OUTER_BOUND ( 'NONE', #5691, .T. ) ;
#19879=CARTESIAN_POINT ( 'NONE',  ( -7.922281120364393914, 4.573931137438271399, -8.047472243342930653 ) ) ;
#19884=VERTEX_POINT ( 'NONE', #18759 ) ;
#19890=CARTESIAN_POINT ( 'NONE',  ( 2.558993250143296372, -7.638875775590942219, -7.593821156097518177 ) ) ;
#19923=CARTESIAN_POINT ( 'NONE',  ( 1.282512619718868541, 8.391164935524033197, -7.795653906408837486 ) ) ;
#19965=CARTESIAN_POINT ( 'NONE',  ( 0.000000000000000000, 0.000000000000000000, -0.5776712190230133270 ) ) ;
#20005=CARTESIAN_POINT ( 'NONE',  ( 0.9763930676190096802, -8.096533237419681228, -7.213065638943101376 ) ) ;
#20013=CARTESIAN_POINT ( 'NONE',  ( 3.750000000000005329, 6.495190528383288253, 0.000000000000000000 ) ) ;
#20022=DIRECTION ( 'NONE',  ( -0.8191520442889907994, 1.003171929053523514E-16, 0.5735764363510474917 ) ) ;
#20032=CARTESIAN_POINT ( 'NONE',  ( 0.000000000000000000, 0.000000000000000000, -0.5776712190230133270 ) ) ;
#20043=CARTESIAN_POINT ( 'NONE',  ( 0.000000000000000000, 0.000000000000000000, 0.000000000000000000 ) ) ;
#20047=B_SPLINE_CURVE_WITH_KNOTS ( 'NONE', 3,
 ( #1341, #10794, #16087, #6666, #14062, #21389 ),
 .UNSPECIFIED., .F., .F.,
 ( 4, 2, 4 ),
 ( 0.000000000000000000, 0.0004189869898914143787, 0.0008379739797828287574 ),
 .UNSPECIFIED. ) ;
#20048=CARTESIAN_POINT ( 'NONE',  ( -0.04725809328185606034, 9.175759667312519241, -8.057670357645360326 ) ) ;
#20069=ORIENTED_EDGE ( 'NONE', *, *, #7652, .T. ) ;
#20074=EDGE_LOOP ( 'NONE', ( #10038, #9751, #9590 ) ) ;
#20097=CARTESIAN_POINT ( 'NONE',  ( -7.500000000000000000, 1.854554393013821745, -0.1880126015361722192 ) ) ;
#20106=CARTESIAN_POINT ( 'NONE',  ( 0.000000000000000000, 0.000000000000000000, -8.499999999999998224 ) ) ;
#20135=EDGE_CURVE ( 'NONE', #5418, #4336, #8458, .T. ) ;
#20138=CARTESIAN_POINT ( 'NONE',  ( -7.894787914004607998, -1.230850257101226302E-13, -7.591390474663425536 ) ) ;
#20141=CARTESIAN_POINT ( 'NONE',  ( -5.000000000000000888, 6.123233995736767268E-16, 0.000000000000000000 ) ) ;
#20145=CARTESIAN_POINT ( 'NONE',  ( -1.015826369459165157, 8.073766409993364590, -7.642786413619490737 ) ) ;
#20154=CARTESIAN_POINT ( 'NONE',  ( -2.249192934210769784E-14, 9.016154170237596688, -7.999534413642735764 ) ) ;
#20180=EDGE_CURVE ( 'NONE', #13071, #6769, #15030, .T. ) ;
#20192=LINE ( 'NONE', #7280, #692 ) ;
#20208=VECTOR ( 'NONE', #22149, 1000.000000000000000 ) ;
#20225=EDGE_CURVE ( 'NONE', #21875, #1621, #14722, .T. ) ;
#20226=DIRECTION ( 'NONE',  ( -0.8660254037844382635, -0.5000000000000004441, 0.000000000000000000 ) ) ;
#20239=CARTESIAN_POINT ( 'NONE',  ( 4.406466114817131796, -6.116179640279303165, -7.446478553994418270 ) ) ;
#20298=VECTOR ( 'NONE', #2049, 1000.000000000000000 ) ;
#20320=AXIS2_PLACEMENT_3D ( 'NONE', #5032, #16512, #12827 ) ;
#20321=EDGE_CURVE ( 'NONE', #16807, #9811, #23637, .T. ) ;
#20323=CARTESIAN_POINT ( 'NONE',  ( 7.500000000000000888, 2.932633423934449812, -0.4709827563909316783 ) ) ;
#20337=CARTESIAN_POINT ( 'NONE',  ( -7.808218555861951238, 4.508077085120201666, -7.999534413642737540 ) ) ;
#20350=CARTESIAN_POINT ( 'NONE',  ( 7.848314987057850800, -4.129027267381569999, -7.493854785173811095 ) ) ;
#20364=CARTESIAN_POINT ( 'NONE',  ( 7.500000000000000000, 4.330127018922190096, -7.422398894150032511 ) ) ;
#20403=B_SPLINE_CURVE_WITH_KNOTS ( 'NONE', 3,
 ( #5251, #9246, #14344, #18054, #21675, #7056, #14799, #5132, #12543 ),
 .UNSPECIFIED., .F., .F.,
 ( 4, 2, 1, 2, 4 ),
 ( 0.000000000000000000, 0.002165063509461097498, 0.004330127018922194995, 0.006495190528383292493, 0.008660254037844389990 ),
 .UNSPECIFIED. ) ;
#20486=CARTESIAN_POINT ( 'NONE',  ( 3.280815508853482498, 7.221948645665444921, -7.591546097228400569 ) ) ;
#20499=CARTESIAN_POINT ( 'NONE',  ( -7.169303301815100227, 4.521054846639364300, -7.349897473154783256 ) ) ;
#20522=CARTESIAN_POINT ( 'NONE',  ( 7.264118654998712898, -4.945491722146229563, -7.907633014911220393 ) ) ;
#20549=CARTESIAN_POINT ( 'NONE',  ( 0.000000000000000000, 0.000000000000000000, 0.000000000000000000 ) ) ;
#20605=DIRECTION ( 'NONE',  ( 0.000000000000000000, 0.000000000000000000, -1.000000000000000000 ) ) ;
#20616=EDGE_CURVE ( 'NONE', #2346, #5614, #7855, .T. ) ;
#20618=UNCERTAINTY_MEASURE_WITH_UNIT (LENGTH_MEASURE( 1.000000000000000082E-05 ), #23236, 'distance_accuracy_value', 'NONE');
#20622=CARTESIAN_POINT ( 'NONE',  ( -4.403473400622099909, -6.117907484625868975, -5.839445138371144960E-15 ) ) ;
#20639=FACE_OUTER_BOUND ( 'NONE', #20074, .T. ) ;
#20660=ADVANCED_FACE ( 'NONE', ( #20639 ), #13090, .T. ) ;
#20692=EDGE_LOOP ( 'NONE', ( #12642, #12768 ) ) ;
#20780=COLOUR_RGB ( '',1.000000000000000000, 0.9490196078431372140, 0.9098039215686274384 ) ;
#20802=ORIENTED_EDGE ( 'NONE', *, *, #9354, .T. ) ;
#20836=CARTESIAN_POINT ( 'NONE',  ( 3.750000000000005329, 6.495190528383288253, 0.000000000000000000 ) ) ;
#20845=CARTESIAN_POINT ( 'NONE',  ( -7.922798540899431252, 4.627424769998836673, -8.057412477672047046 ) ) ;
#20849=EDGE_CURVE ( 'NONE', #16807, #18546, #15879, .T. ) ;
#20861=ORIENTED_EDGE ( 'NONE', *, *, #11631, .T. ) ;
#20877=EDGE_CURVE ( 'NONE', #1864, #19450, #21148, .T. ) ;
#20892=EDGE_LOOP ( 'NONE', ( #9519, #16044, #4345, #10305 ) ) ;
#20899=CARTESIAN_POINT ( 'NONE',  ( -2.387978478801491278, -7.281554020289322970, -7.069802615102039667 ) ) ;
#20904=AXIS2_PLACEMENT_3D ( 'NONE', #7748, #499, #4095 ) ;
#20908=ORIENTED_EDGE ( 'NONE', *, *, #6969, .F. ) ;
#20932=EDGE_CURVE ( 'NONE', #11056, #4336, #7189, .T. ) ;
#20940=EDGE_LOOP ( 'NONE', ( #14594, #12513, #22171, #10927 ) ) ;
#20973=ADVANCED_FACE ( 'NONE', ( #23735 ), #1870, .T. ) ;
#21015=CARTESIAN_POINT ( 'NONE',  ( 7.922281120364393914, -4.573931137438282057, -8.047472243342932430 ) ) ;
#21026=CARTESIAN_POINT ( 'NONE',  ( 7.500000000000000888, 1.443375672974060109, -7.063244554130000630 ) ) ;
#21040=EDGE_LOOP ( 'NONE', ( #8514, #14415, #11114, #12998, #13652, #1563 ) ) ;
#21052=DIRECTION ( 'NONE',  ( -1.000000000000000000, 0.000000000000000000, 0.000000000000000000 ) ) ;
#21095=EDGE_LOOP ( 'NONE', ( #3176, #8218, #21821, #3600 ) ) ;
#21098=B_SPLINE_CURVE_WITH_KNOTS ( 'NONE', 3,
 ( #13017, #3657, #70, #7421, #14806, #22137, #20323, #9817, #3781, #7993 ),
 .UNSPECIFIED., .F., .F.,
 ( 4, 2, 2, 2, 4 ),
 ( 0.01051144076094935251, 0.01162027323572611265, 0.01272910571050287452, 0.01383793818527963640, 0.01494677066005639827 ),
 .UNSPECIFIED. ) ;
#21103=CARTESIAN_POINT ( 'NONE',  ( -3.750000000000007105, -6.495190528383289141, 0.000000000000000000 ) ) ;
#21135=CARTESIAN_POINT ( 'NONE',  ( -3.295171437451516638, -7.213553046160524396, -7.590212325761481971 ) ) ;
#21148=CIRCLE ( 'NONE', #3399, 5.000000000000000888 ) ;
#21159=ORIENTED_EDGE ( 'NONE', *, *, #22133, .T. ) ;
#21168=CARTESIAN_POINT ( 'NONE',  ( 7.499999999999999112, 4.652409454067514716, -7.929128589908465585 ) ) ;
#21220=PLANE ( 'NONE',  #21562 ) ;
#21241=CARTESIAN_POINT ( 'NONE',  ( -7.025762299539908296E-16, -8.895730773063899477, -7.917997657324741034 ) ) ;
#21254=CARTESIAN_POINT ( 'NONE',  ( -7.922281120364393914, -4.573931137438277617, -8.047472243342932430 ) ) ;
#21293=CARTESIAN_POINT ( 'NONE',  ( 7.499999999999999112, -1.614186302720606481, -7.450236204328171574 ) ) ;
#21320=PLANE ( 'NONE',  #7334 ) ;
#21352=AXIS2_PLACEMENT_3D ( 'NONE', #19726, #10584, #17923 ) ;
#21372=ADVANCED_FACE ( 'NONE', ( #18168 ), #19621, .F. ) ;
#21381=CARTESIAN_POINT ( 'NONE',  ( 7.968863443239234456, 4.547634245050474533, -8.057411785091787237 ) ) ;
#21389=CARTESIAN_POINT ( 'NONE',  ( 7.922281120364393914, -4.573931137438282057, -8.047472243342932430 ) ) ;
#21404=FACE_OUTER_BOUND ( 'NONE', #438, .T. ) ;
#21436=DIRECTION ( 'NONE',  ( -0.8191520442889907994, 0.000000000000000000, -0.5735764363510474917 ) ) ;
#21459=CARTESIAN_POINT ( 'NONE',  ( -1.994931997373328159E-14, -8.660254037844390851, -1.000000000000000888 ) ) ;
#21469=B_SPLINE_CURVE_WITH_KNOTS ( 'NONE', 3,
 ( #12941, #5530, #5421, #16408, #23756, #14602 ),
 .UNSPECIFIED., .F., .F.,
 ( 4, 2, 4 ),
 ( 0.000000000000000000, 0.0004189869898914161677, 0.0008379739797828302753 ),
 .UNSPECIFIED. ) ;
#21487=CARTESIAN_POINT ( 'NONE',  ( -4.599534470795546781, 6.460478697738500031, -7.590212325761530821 ) ) ;
#21526=CARTESIAN_POINT ( 'NONE',  ( 7.500000000000001776, 0.000000000000000000, 0.000000000000000000 ) ) ;
#21558=( NAMED_UNIT ( * ) SI_UNIT ( $, .STERADIAN. ) SOLID_ANGLE_UNIT ( ) );
#21562=AXIS2_PLACEMENT_3D ( 'NONE', #3193, #4676, #14232 ) ;
#21582=VERTEX_POINT ( 'NONE', #16225 ) ;
#21585=CARTESIAN_POINT ( 'NONE',  ( 5.047120108843200725, -5.746297884371399434, -0.1007566405101860824 ) ) ;
#21636=CARTESIAN_POINT ( 'NONE',  ( 2.387978478801324300, 7.281554020289410012, -7.069802615102035226 ) ) ;
#21648=ORIENTED_EDGE ( 'NONE', *, *, #20877, .T. ) ;
#21675=CARTESIAN_POINT ( 'NONE',  ( -7.500000000000000000, -3.469446951953614189E-15, -6.991905250253751980 ) ) ;
#21717=CIRCLE ( 'NONE', #13679, 0.7733184030943203169 ) ;
#21719=ORIENTED_EDGE ( 'NONE', *, *, #14182, .T. ) ;
#21724=CARTESIAN_POINT ( 'NONE',  ( -4.174999999999999822, 5.112900386440199535E-16, -0.5776712190230133270 ) ) ;
#21794=CARTESIAN_POINT ( 'NONE',  ( 0.000000000000000000, 0.000000000000000000, 0.000000000000000000 ) ) ;
#21797=ORIENTED_EDGE ( 'NONE', *, *, #9440, .F. ) ;
#21821=ORIENTED_EDGE ( 'NONE', *, *, #7257, .T. ) ;
#21875=VERTEX_POINT ( 'NONE', #20364 ) ;
#21908=ORIENTED_EDGE ( 'NONE', *, *, #14537, .F. ) ;
#21975=CARTESIAN_POINT ( 'NONE',  ( 2.547548355748054857E-16, 8.895721644649732696, -7.917989418073286600 ) ) ;
#21980=EDGE_CURVE ( 'NONE', #21875, #5970, #21469, .T. ) ;
#22045=DIRECTION ( 'NONE',  ( -0.5000000000000005551, 0.8660254037844383745, 0.000000000000000000 ) ) ;
#22061=LINE ( 'NONE', #16755, #14288 ) ;
#22084=CARTESIAN_POINT ( 'NONE',  ( -6.602753909532903975, -5.319290460493544259, -7.792447862505333056 ) ) ;
#22130=CARTESIAN_POINT ( 'NONE',  ( -7.500000000000001776, 0.000000000000000000, 0.000000000000000000 ) ) ;
#22133=EDGE_CURVE ( 'NONE', #7849, #13071, #17155, .T. ) ;
#22136=EDGE_CURVE ( 'NONE', #23462, #7849, #309, .T. ) ;
#22137=CARTESIAN_POINT ( 'NONE',  ( 7.499999999999999112, 2.575910028905302074, -0.3641256808890108720 ) ) ;
#22149=DIRECTION ( 'NONE',  ( -0.000000000000000000, -0.000000000000000000, 1.000000000000000000 ) ) ;
#22166=CARTESIAN_POINT ( 'NONE',  ( 5.112021521198788498, -5.708827036477115868, -7.069802615102037890 ) ) ;
#22171=ORIENTED_EDGE ( 'NONE', *, *, #12155, .F. ) ;
#22185=CARTESIAN_POINT ( 'NONE',  ( -7.779103221381273414, 4.168986698926021361, -7.929128246061903695 ) ) ;
#22205=DIRECTION ( 'NONE',  ( -0.000000000000000000, -0.000000000000000000, 1.000000000000000000 ) ) ;
#22235=ORIENTED_EDGE ( 'NONE', *, *, #8843, .F. ) ;
#22267=LINE ( 'NONE', #7668, #20208 ) ;
#22275=CARTESIAN_POINT ( 'NONE',  ( 0.000000000000000000, 0.000000000000000000, 0.000000000000000000 ) ) ;
#22279=CARTESIAN_POINT ( 'NONE',  ( -7.500000000000000000, -1.572902445675612659, -7.069816568113127531 ) ) ;
#22294=TOROIDAL_SURFACE ( 'NONE', #6109, 10.12668159690567649, 0.7733184030943209830 ) ;
#22300=AXIS2_PLACEMENT_3D ( 'NONE', #1400, #23509, #1632 ) ;
#22325=AXIS2_PLACEMENT_3D ( 'NONE', #20549, #22372, #9711 ) ;
#22335=CARTESIAN_POINT ( 'NONE',  ( -5.274401269815139237, -6.074457022762090652, -7.633824513837113912 ) ) ;
#22372=DIRECTION ( 'NONE',  ( 0.000000000000000000, 0.000000000000000000, 1.000000000000000000 ) ) ;
#22381=ORIENTED_EDGE ( 'NONE', *, *, #15203, .F. ) ;
#22407=CARTESIAN_POINT ( 'NONE',  ( -7.500000000000346390, -3.105855721450154316, -7.659356991636309786 ) ) ;
#22420=CARTESIAN_POINT ( 'NONE',  ( 2.621086668468698644, 7.606368536631364030, -7.634085501268425666 ) ) ;
#22431=CARTESIAN_POINT ( 'NONE',  ( 4.250000000000000000, 0.000000000000000000, -0.5251556536572846712 ) ) ;
#22437=EDGE_CURVE ( 'NONE', #19785, #16807, #10551, .T. ) ;
#22517=CARTESIAN_POINT ( 'NONE',  ( -7.894955577759523280, 1.603085139988202901, -7.593799241562120272 ) ) ;
#22521=ORIENTED_EDGE ( 'NONE', *, *, #3190, .T. ) ;
#22536=FACE_OUTER_BOUND ( 'NONE', #17496, .T. ) ;
#22537=EDGE_CURVE ( 'NONE', #11056, #7557, #20192, .T. ) ;
#22589=CARTESIAN_POINT ( 'NONE',  ( 7.499999999999999112, -1.443375672974070323, -7.063244554130001518 ) ) ;
#22592=ADVANCED_FACE ( 'NONE', ( #7049 ), #7246, .F. ) ;
#22622=EDGE_LOOP ( 'NONE', ( #19636, #18945, #2717, #1184 ) ) ;
#22637=CARTESIAN_POINT ( 'NONE',  ( -4.250000000000000000, 5.204748896376250699E-16, -0.5251556536572846712 ) ) ;
#22639=CARTESIAN_POINT ( 'NONE',  ( -7.499999999999999112, 4.651022038490018495, -7.928862870699868282 ) ) ;
#22647=ORIENTED_EDGE ( 'NONE', *, *, #14352, .F. ) ;
#22655=CARTESIAN_POINT ( 'NONE',  ( 0.000000000000000000, 0.000000000000000000, 0.000000000000000000 ) ) ;
#22697=CARTESIAN_POINT ( 'NONE',  ( 5.276765049035074817, -6.073111908730307817, -7.634085501268428331 ) ) ;
#22702=CARTESIAN_POINT ( 'NONE',  ( 0.04725809328185039127, -9.175759667312528123, -8.057670357645362103 ) ) ;
#22760=CARTESIAN_POINT ( 'NONE',  ( 4.250000000000000000, 0.000000000000000000, -9.449444346342714240 ) ) ;
#22799=UNCERTAINTY_MEASURE_WITH_UNIT (LENGTH_MEASURE( 1.000000000000000082E-05 ), #6970, 'distance_accuracy_value', 'NONE');
#22820=CARTESIAN_POINT ( 'NONE',  ( -1.060314165522979968, -8.048081368954337123, -7.659344964963557878 ) ) ;
#22832=ADVANCED_FACE ( 'NONE', ( #14284 ), #12721, .F. ) ;
#22839=CARTESIAN_POINT ( 'NONE',  ( -6.601567268551443490, 5.319966374295965750, -7.792327460285856766 ) ) ;
#22847=CARTESIAN_POINT ( 'NONE',  ( 7.500000000000000000, -3.202733125947433201, -7.213074474936314928 ) ) ;
#22865=ADVANCED_FACE ( 'NONE', ( #23765 ), #22294, .T. ) ;
#22930=ADVANCED_FACE ( 'NONE', ( #10767 ), #4017, .F. ) ;
#22940=B_SPLINE_CURVE_WITH_KNOTS ( 'NONE', 3,
 ( #20836, #9979, #15421, #10214, #2721, #551 ),
 .UNSPECIFIED., .F., .F.,
 ( 4, 2, 4 ),
 ( 0.004444412883774346255, 0.006655097293744437204, 0.008865781703714529019 ),
 .UNSPECIFIED. ) ;
#22995=SHAPE_REPRESENTATION ( 'hex flange nut gradea_iso_ISO - 4161 - M10 - N', ( #11210 ), #370 ) ;
#23056=ORIENTED_EDGE ( 'NONE', *, *, #19479, .T. ) ;
#23060=VERTEX_POINT ( 'NONE', #2752 ) ;
#23077=CARTESIAN_POINT ( 'NONE',  ( -4.613983237546153582, 6.452243898629808960, -7.591546097228401457 ) ) ;
#23108=VECTOR ( 'NONE', #19359, 1000.000000000000000 ) ;
#23193=FACE_OUTER_BOUND ( 'NONE', #15757, .T. ) ;
#23196=CARTESIAN_POINT ( 'NONE',  ( 5.000000000000000888, 0.000000000000000000, -10.00000000000000000 ) ) ;
#23210=CARTESIAN_POINT ( 'NONE',  ( 7.500000000000000000, 3.160172554975063886, -7.231829826456836585 ) ) ;
#23214=LINE ( 'NONE', #19346, #14658 ) ;
#23217=CARTESIAN_POINT ( 'NONE',  ( 7.499999999999999112, -2.930060224340428565, -0.4701183149080248036 ) ) ;
#23236=( LENGTH_UNIT ( ) NAMED_UNIT ( * ) SI_UNIT ( .MILLI., .METRE. ) );
#23277=DIRECTION ( 'NONE',  ( 0.000000000000000000, -1.000000000000000000, 0.000000000000000000 ) ) ;
#23284=CARTESIAN_POINT ( 'NONE',  ( -7.894787914004607998, -0.7661396099416333261, -7.591390474663429089 ) ) ;
#23290=CARTESIAN_POINT ( 'NONE',  ( 0.000000000000000000, 0.000000000000000000, -9.974600000000000577 ) ) ;
#23306=CARTESIAN_POINT ( 'NONE',  ( 3.093533885183100018, 6.874201416487501604, -7.446478553995813598 ) ) ;
#23318=CARTESIAN_POINT ( 'NONE',  ( -7.264118654998712010, 4.945491722146218905, -7.907633014911216840 ) ) ;
#23321=CARTESIAN_POINT ( 'NONE',  ( -7.500000000000000000, -2.571118828324945760, -0.3627527587569098766 ) ) ;
#23329=CARTESIAN_POINT ( 'NONE',  ( -6.874999999999995559, 4.690970937165706900, -7.298562697733101068 ) ) ;
#23361=FILL_AREA_STYLE_COLOUR ( '', #20780 ) ;
#23367=LINE ( 'NONE', #6826, #9991 ) ;
#23384=CARTESIAN_POINT ( 'NONE',  ( 7.499999999999999112, -4.330127018922205195, -1.000000000000000888 ) ) ;
#23388=DIRECTION ( 'NONE',  ( -1.000000000000000000, 0.000000000000000000, 0.000000000000000000 ) ) ;
#23395=CARTESIAN_POINT ( 'NONE',  ( -4.232971792145048787E-15, -9.016621985895911351, -7.999704684617487516 ) ) ;
#23415=DIRECTION ( 'NONE',  ( -0.000000000000000000, -0.000000000000000000, 1.000000000000000000 ) ) ;
#23459=ORIENTED_EDGE ( 'NONE', *, *, #219, .T. ) ;
#23462=VERTEX_POINT ( 'NONE', #1994 ) ;
#23485=DIRECTION ( 'NONE',  ( 1.000000000000000000, 0.000000000000000000, 0.000000000000000000 ) ) ;
#23486=CARTESIAN_POINT ( 'NONE',  ( 7.922281120364393914, -4.573931137438282057, -8.047472243342932430 ) ) ;
#23509=DIRECTION ( 'NONE',  ( 0.000000000000000000, 0.000000000000000000, -1.000000000000000000 ) ) ;
#23545=ORIENTED_EDGE ( 'NONE', *, *, #17713, .F. ) ;
#23589=ORIENTED_EDGE ( 'NONE', *, *, #11441, .T. ) ;
#23600=CARTESIAN_POINT ( 'NONE',  ( -7.499999999999999112, 0.3744244963005040061, 1.590163186312071526E-15 ) ) ;
#23629=ORIENTED_EDGE ( 'NONE', *, *, #19153, .T. ) ;
#23637=B_SPLINE_CURVE_WITH_KNOTS ( 'NONE', 3,
 ( #8246, #23318, #22839, #15512, #23077, #2901, #15621, #13961, #4853, #4375 ),
 .UNSPECIFIED., .F., .F.,
 ( 4, 2, 2, 2, 4 ),
 ( 0.000000000000000000, 0.002305503304226491634, 0.004611006608452983269, 0.006916509912679474036, 0.009222013216905963068 ),
 .UNSPECIFIED. ) ;
#23656=VERTEX_POINT ( 'NONE', #22637 ) ;
#23659=B_SPLINE_CURVE_WITH_KNOTS ( 'NONE', 3,
 ( #6052, #15501, #9252, #22589, #8233, #21026, #7533, #6296, #19202 ),
 .UNSPECIFIED., .F., .F.,
 ( 4, 2, 1, 2, 4 ),
 ( 0.000000000000000000, 0.002165063509461097498, 0.004330127018922194995, 0.006495190528383292493, 0.008660254037844389990 ),
 .UNSPECIFIED. ) ;
#23709=CIRCLE ( 'NONE', #7133, 7.500000000000001776 ) ;
#23734=EDGE_CURVE ( 'NONE', #13071, #19884, #19099, .T. ) ;
#23735=FACE_OUTER_BOUND ( 'NONE', #15750, .T. ) ;
#23746=CARTESIAN_POINT ( 'NONE',  ( 5.276498195232308674, -6.073236878017951312, -7.633618187056764981 ) ) ;
#23756=CARTESIAN_POINT ( 'NONE',  ( 7.808623696107343193, 4.508310992947586193, -7.999704684617482187 ) ) ;
#23765=FACE_OUTER_BOUND ( 'NONE', #20892, .T. ) ;
#23770=EDGE_CURVE ( 'NONE', #11056, #8135, #4990, .T. ) ;
#23774=( BOUNDED_SURFACE ( )  B_SPLINE_SURFACE ( 3, 2, ( 
 ( #1116, #8256, #19343 ),
 ( #22847, #17319, #768 ),
 ( #15743, #21293, #10093 ),
 ( #10453, #11914, #17432 ),
 ( #876, #17794, #6432 ),
 ( #23210, #8368, #14073 ),
 ( #8612, #2802, #8148 ),
 ( #15521, #21168, #4636 ) ),
 .UNSPECIFIED., .F., .F., .F. ) 
 B_SPLINE_SURFACE_WITH_KNOTS ( ( 4, 2, 2, 4 ),
 ( 3, 3 ),
 ( 0.03850042371095789562, 0.04313406099830585649, 0.04545087964197984387, 0.04776769828565382431 ),
 ( 0.000000000000000000, 1.000000000000000000 ),
 .UNSPECIFIED. ) 
 GEOMETRIC_REPRESENTATION_ITEM ( )  RATIONAL_B_SPLINE_SURFACE ( (
 ( 1.000000000000000000, 0.8047781847388135734, 1.000000000000000000),
 ( 1.000000000000000000, 0.8123760230793541925, 1.000000000000000000),
 ( 1.000000000000000000, 0.8190653851695529619, 1.000000000000000000),
 ( 1.000000000000000000, 0.8191940386278896424, 1.000000000000000000),
 ( 1.000000000000000000, 0.8176096570055705337, 1.000000000000000000),
 ( 1.000000000000000000, 0.8122964723277524834, 1.000000000000000000),
 ( 1.000000000000000000, 0.8086312464132844324, 1.000000000000000000),
 ( 1.000000000000000000, 0.8047712192439641088, 1.000000000000000000) ) ) 
 REPRESENTATION_ITEM ( '' )  SURFACE ( )  );
#23780=CARTESIAN_POINT ( 'NONE',  ( 0.3306966981845720355, 8.469326210127405830, -7.349897473153450989 ) ) ;
#23921=COLOUR_RGB('Black',0.12,0.14,0.17);
#23922=FILL_AREA_STYLE_COLOUR('',#23921);
#23923=FILL_AREA_STYLE('',(#23922));
#23924=SURFACE_STYLE_FILL_AREA(#23923);
#23925=SURFACE_SIDE_STYLE('',(#23924));
#23926=SURFACE_STYLE_USAGE(.BOTH.,#23925);
#23927=PRESENTATION_STYLE_ASSIGNMENT((#23926));
ENDSEC;
END-ISO-10303-21;
